ISO-10303-21;
HEADER;
FILE_DESCRIPTION (('STEP AP214'),
    '1' );
FILE_NAME ('11. Nut M10.step',
    '2026-10-09T08:13:37',
    ( '' ),
    ( '' ),
    'SwSTEP 2.0',
    'SolidWorks 2021',
    '' );
FILE_SCHEMA (( 'AUTOMOTIVE_DESIGN' ));
ENDSEC;

DATA;
#7=CARTESIAN_POINT ( 'NONE',  ( 8.690363669209105524, -2.361802048420730493, 2.947848588679143234 ) ) ;
#129=CARTESIAN_POINT ( 'NONE',  ( -5.603096392576914830, -1.514639124457109354, 8.295152368350901639 ) ) ;
#510=VECTOR ( 'NONE', #3553, 1000.000000000000000 ) ;
#548=DIRECTION ( 'NONE',  ( 0.000000000000000000, 0.000000000000000000, -1.000000000000000000 ) ) ;
#566=DIRECTION ( 'NONE',  ( 0.000000000000000000, 1.000000000000000000, 0.000000000000000000 ) ) ;
#625=CARTESIAN_POINT ( 'NONE',  ( -6.887213563469350319, -2.329718218673038077, -6.070996185493596542 ) ) ;
#678=CARTESIAN_POINT ( 'NONE',  ( 0.000000000000000000, 2.500000000000000000, 0.000000000000000000 ) ) ;
#704=CARTESIAN_POINT ( 'NONE',  ( 9.566487832665400148, -1.863712308906143811, 1.430357023834058161 ) ) ;
#924=CARTESIAN_POINT ( 'NONE',  ( -8.246138225238285102, -2.499999999999994671, -3.717269627651451191 ) ) ;
#961=PLANE ( 'NONE',  #9583 ) ;
#1005=CARTESIAN_POINT ( 'NONE',  ( 6.123233995736766282E-16, -1.999999999999995337, -5.000000000000000000 ) ) ;
#1050=DIRECTION ( 'NONE',  ( 0.000000000000000000, 0.000000000000000000, 1.000000000000000000 ) ) ;
#1218=AXIS2_PLACEMENT_3D ( 'NONE', #48330, #21556, #43071 ) ;
#1240=DIRECTION ( 'NONE',  ( 0.000000000000000000, 0.000000000000000000, -1.000000000000000000 ) ) ;
#1549=ORIENTED_EDGE ( 'NONE', *, *, #58572, .F. ) ;
#1557=CARTESIAN_POINT ( 'NONE',  ( 0.000000000000000000, -2.500000000000000000, 0.000000000000000000 ) ) ;
#1899=ORIENTED_EDGE ( 'NONE', *, *, #69263, .T. ) ;
#2172=CONICAL_SURFACE ( 'NONE', #41544, 9.000000000000000000, 0.7853981633974500554 ) ;
#2235=CARTESIAN_POINT ( 'NONE',  ( 6.735557395310448926E-16, -2.500000000000000000, 5.500000000000005329 ) ) ;
#2291=CARTESIAN_POINT ( 'NONE',  ( 8.252730563585672030, 2.464278740834330517, -3.705851362693084905 ) ) ;
#2403=AXIS2_PLACEMENT_3D ( 'NONE', #31743, #9970, #15606 ) ;
#2462=CARTESIAN_POINT ( 'NONE',  ( -1.502314598737159031E-15, -2.500000000000000000, -9.000000000000000000 ) ) ;
#2486=AXIS2_PLACEMENT_3D ( 'NONE', #23252, #55606, #39809 ) ;
#2551=DIRECTION ( 'NONE',  ( 0.000000000000000000, 1.000000000000000000, 0.000000000000000000 ) ) ;
#2605=LINE ( 'NONE', #19518, #51190 ) ;
#2639=CARTESIAN_POINT ( 'NONE',  ( 5.196152422706628471, -1.107695154586738173, -9.000000000000005329 ) ) ;
#2645=CARTESIAN_POINT ( 'NONE',  ( 0.000000000000000000, -2.500000000000000000, 0.000000000000000000 ) ) ;
#2702=ORIENTED_EDGE ( 'NONE', *, *, #38026, .F. ) ;
#2766=DIRECTION ( 'NONE',  ( 0.000000000000000000, 0.000000000000000000, 1.000000000000000000 ) ) ;
#2806=B_SPLINE_CURVE_WITH_KNOTS ( 'NONE', 3,
 ( #38700, #924, #61140, #49919, #60101, #12947 ),
 .UNSPECIFIED., .F., .F.,
 ( 4, 2, 4 ),
 ( 0.005386537104126974673, 0.008060814333094815098, 0.01073509156206265379 ),
 .UNSPECIFIED. ) ;
#2841=FILL_AREA_STYLE ('',( #34893 ) ) ;
#2944=DIRECTION ( 'NONE',  ( -0.000000000000000000, -1.000000000000000000, -0.000000000000000000 ) ) ;
#3008=CARTESIAN_POINT ( 'NONE',  ( -3.542344102440325049, -1.863645424029197750, -9.000000000000007105 ) ) ;
#3028=EDGE_CURVE ( 'NONE', #20287, #33218, #57843, .T. ) ;
#3170=( LENGTH_UNIT ( ) NAMED_UNIT ( * ) SI_UNIT ( .MILLI., .METRE. ) );
#3204=ORIENTED_EDGE ( 'NONE', *, *, #43657, .T. ) ;
#3209=EDGE_CURVE ( 'NONE', #53612, #18297, #46390, .T. ) ;
#3226=ORIENTED_EDGE ( 'NONE', *, *, #64346, .T. ) ;
#3235=MANIFOLD_SOLID_BREP ( 'Chamfer1', #16079 ) ;
#3360=CARTESIAN_POINT ( 'NONE',  ( -0.2278693232858696738, -2.499999999999995115, -9.000000000000007105 ) ) ;
#3444=ADVANCED_FACE ( 'NONE', ( #15587 ), #35018, .F. ) ;
#3463=ORIENTED_EDGE ( 'NONE', *, *, #12220, .T. ) ;
#3510=CARTESIAN_POINT ( 'NONE',  ( 0.000000000000000000, 2.500000000000000000, 0.000000000000000000 ) ) ;
#3540=DIRECTION ( 'NONE',  ( 0.000000000000000000, 1.000000000000000000, 0.000000000000000000 ) ) ;
#3553=DIRECTION ( 'NONE',  ( -0.000000000000000000, -1.000000000000000000, -0.000000000000000000 ) ) ;
#3626=EDGE_LOOP ( 'NONE', ( #45453, #66203, #21867, #19728, #39538, #25276 ) ) ;
#3643=CARTESIAN_POINT ( 'NONE',  ( 7.566679973970428463, -2.499999999999998224, 4.894125840469273570 ) ) ;
#3654=CARTESIAN_POINT ( 'NONE',  ( -1.502314598737159031E-15, -2.500000000000000000, -9.000000000000000000 ) ) ;
#3723=CARTESIAN_POINT ( 'NONE',  ( -1.502314598737159031E-15, -2.500000000000000000, -9.000000000000000000 ) ) ;
#3724=ORIENTED_EDGE ( 'NONE', *, *, #61532, .T. ) ;
#3732=ORIENTED_EDGE ( 'NONE', *, *, #23555, .F. ) ;
#3801=ADVANCED_FACE ( 'NONE', ( #31651 ), #15459, .T. ) ;
#3928=DIRECTION ( 'NONE',  ( 0.000000000000000000, 0.000000000000000000, 1.000000000000000000 ) ) ;
#3937=DIRECTION ( 'NONE',  ( 0.000000000000000000, 0.000000000000000000, 1.000000000000000000 ) ) ;
#3947=ORIENTED_EDGE ( 'NONE', *, *, #33286, .T. ) ;
#4004=DIRECTION ( 'NONE',  ( -0.000000000000000000, -1.000000000000000000, -0.000000000000000000 ) ) ;
#4106=LINE ( 'NONE', #8393, #14309 ) ;
#4128=DIRECTION ( 'NONE',  ( 0.5000000000000002220, 0.000000000000000000, 0.8660254037844384856 ) ) ;
#4258=CARTESIAN_POINT ( 'NONE',  ( 0.000000000000000000, -2.500000000000000000, 0.000000000000000000 ) ) ;
#4344=VERTEX_POINT ( 'NONE', #10811 ) ;
#4437=CARTESIAN_POINT ( 'NONE',  ( -7.794228634059948035, 2.500000000000000000, 4.499999999999999112 ) ) ;
#4542=CARTESIAN_POINT ( 'NONE',  ( 8.246138225238281549, 2.499999999999997780, 3.717269627651450303 ) ) ;
#4667=FACE_OUTER_BOUND ( 'NONE', #57367, .T. ) ;
#4822=CARTESIAN_POINT ( 'NONE',  ( 5.196152422706631135, 1.107695154586740394, 9.000000000000001776 ) ) ;
#4851=CARTESIAN_POINT ( 'NONE',  ( 0.000000000000000000, -2.500000000000000000, 0.000000000000000000 ) ) ;
#4917=DIRECTION ( 'NONE',  ( 0.000000000000000000, 0.000000000000000000, 1.000000000000000000 ) ) ;
#5239=CARTESIAN_POINT ( 'NONE',  ( -2.243484957755116582, 2.233878551459170136, 9.000000000000005329 ) ) ;
#5348=CARTESIAN_POINT ( 'NONE',  ( 0.000000000000000000, 2.500000000000000000, 0.000000000000000000 ) ) ;
#5390=AXIS2_PLACEMENT_3D ( 'NONE', #9681, #4004, #52248 ) ;
#5404=CARTESIAN_POINT ( 'NONE',  ( 1.802043943559354711, -2.359472279213376211, 9.000000000000003553 ) ) ;
#5483=SURFACE_STYLE_FILL_AREA ( #54039 ) ;
#5550=DIRECTION ( 'NONE',  ( 0.000000000000000000, 0.000000000000000000, 1.000000000000000000 ) ) ;
#5572=CARTESIAN_POINT ( 'NONE',  ( 10.39230484541326582, 1.107695154586738839, 1.440973567693753677E-18 ) ) ;
#5616=AXIS2_PLACEMENT_3D ( 'NONE', #36589, #31229, #67865 ) ;
#5692=FACE_OUTER_BOUND ( 'NONE', #15423, .T. ) ;
#5730=DIRECTION ( 'NONE',  ( 1.000000000000000000, 0.000000000000000000, -1.669238443041287922E-16 ) ) ;
#6016=ORIENTED_EDGE ( 'NONE', *, *, #60829, .T. ) ;
#6024=FACE_BOUND ( 'NONE', #62864, .T. ) ;
#6053=CARTESIAN_POINT ( 'NONE',  ( 10.39230484541326582, -1.107695154586738839, 1.440973567693753677E-18 ) ) ;
#6093=PLANE ( 'NONE',  #57341 ) ;
#6099=CONICAL_SURFACE ( 'NONE', #30797, 9.000000000000000000, 0.7853981633974500554 ) ;
#6135=ORIENTED_EDGE ( 'NONE', *, *, #19275, .T. ) ;
#6136=ADVANCED_FACE ( 'NONE', ( #41281 ), #68684, .F. ) ;
#6210=DIRECTION ( 'NONE',  ( 0.000000000000000000, 0.000000000000000000, 1.000000000000000000 ) ) ;
#6216=CARTESIAN_POINT ( 'NONE',  ( 5.196152422706628471, 1.107695154586738173, -9.000000000000005329 ) ) ;
#6236=FACE_OUTER_BOUND ( 'NONE', #55636, .T. ) ;
#6323=CARTESIAN_POINT ( 'NONE',  ( -6.020204320972970535, 1.861307952554190903, -7.572700244129129565 ) ) ;
#6436=FACE_OUTER_BOUND ( 'NONE', #25939, .T. ) ;
#6529=DIRECTION ( 'NONE',  ( 0.000000000000000000, 1.000000000000000000, 0.000000000000000000 ) ) ;
#6579=DIRECTION ( 'NONE',  ( 0.000000000000000000, 0.000000000000000000, 1.000000000000000000 ) ) ;
#6740=CARTESIAN_POINT ( 'NONE',  ( -6.021969435454500363, 1.863712308906140258, 7.569642976165947168 ) ) ;
#6761=EDGE_CURVE ( 'NONE', #13621, #18297, #2806, .T. ) ;
#6772=ORIENTED_EDGE ( 'NONE', *, *, #40622, .F. ) ;
#6781=PLANE ( 'NONE',  #10602 ) ;
#6792=CIRCLE ( 'NONE', #39432, 9.000000000000000000 ) ;
#7137=AXIS2_PLACEMENT_3D ( 'NONE', #37199, #58262, #10086 ) ;
#7149=ADVANCED_FACE ( 'NONE', ( #32954 ), #22797, .T. ) ;
#7217=DIRECTION ( 'NONE',  ( 0.000000000000000000, 0.000000000000000000, 1.000000000000000000 ) ) ;
#7336=ORIENTED_EDGE ( 'NONE', *, *, #41987, .T. ) ;
#7375=DIRECTION ( 'NONE',  ( 0.5000000000000000000, 0.000000000000000000, -0.8660254037844385966 ) ) ;
#7381=CARTESIAN_POINT ( 'NONE',  ( -6.667623377008405683, 2.231456886122025196, -6.451337545287480602 ) ) ;
#7383=CARTESIAN_POINT ( 'NONE',  ( 0.000000000000000000, 1.999999999999998668, 0.000000000000000000 ) ) ;
#7539=AXIS2_PLACEMENT_3D ( 'NONE', #46934, #8305, #68695 ) ;
#7612=EDGE_CURVE ( 'NONE', #23616, #13621, #55749, .T. ) ;
#7638=AXIS2_PLACEMENT_3D ( 'NONE', #46681, #45956, #62452 ) ;
#7644=CARTESIAN_POINT ( 'NONE',  ( 4.383776131304280455, 1.496531397472844693, 9.000000000000003553 ) ) ;
#7757=DIRECTION ( 'NONE',  ( 0.000000000000000000, 0.000000000000000000, 1.000000000000000000 ) ) ;
#7848=DIRECTION ( 'NONE',  ( -8.881784197001252323E-16, 0.000000000000000000, 1.000000000000000000 ) ) ;
#7992=CARTESIAN_POINT ( 'NONE',  ( 8.021777294149467608, 2.499999999999998224, -4.105874159530731760 ) ) ;
#8019=CARTESIAN_POINT ( 'NONE',  ( -0.9109038252169192607, 2.456844516558473135, 9.000000000000001776 ) ) ;
#8263=ADVANCED_FACE ( 'NONE', ( #46787 ), #47834, .F. ) ;
#8305=DIRECTION ( 'NONE',  ( 0.000000000000000000, 0.000000000000000000, -1.000000000000000000 ) ) ;
#8393=CARTESIAN_POINT ( 'NONE',  ( 0.000000000000000000, -2.500000000000000000, -5.500000000000005329 ) ) ;
#8712=VERTEX_POINT ( 'NONE', #58936 ) ;
#8732=DIRECTION ( 'NONE',  ( -0.8660254037844385966, 0.000000000000000000, -0.5000000000000003331 ) ) ;
#8821=B_SPLINE_CURVE_WITH_KNOTS ( 'NONE', 3,
 ( #4822, #47813, #42505, #37236, #25243, #58642, #10469, #46399 ),
 .UNSPECIFIED., .F., .F.,
 ( 4, 2, 2, 4 ),
 ( 2.544313220888523934E-07, 0.002693395767724531854, 0.004039966435925753697, 0.005386537104126975541 ),
 .UNSPECIFIED. ) ;
#8877=CARTESIAN_POINT ( 'NONE',  ( -5.196152422706636465, 2.500000000000000000, -9.000000000000003553 ) ) ;
#8978=DIRECTION ( 'NONE',  ( -0.000000000000000000, 1.000000000000000000, -0.000000000000000000 ) ) ;
#8979=EDGE_CURVE ( 'NONE', #60124, #56915, #37525, .T. ) ;
#9208=CARTESIAN_POINT ( 'NONE',  ( -10.39230484541326938, 2.500000000000000000, -1.734723475976807094E-15 ) ) ;
#9222=EDGE_CURVE ( 'NONE', #63169, #16904, #54950, .T. ) ;
#9228=CARTESIAN_POINT ( 'NONE',  ( 0.000000000000000000, 2.500000000000000000, 0.000000000000000000 ) ) ;
#9548=CARTESIAN_POINT ( 'NONE',  ( -5.196152422706636465, 1.107695154586736175, -9.000000000000003553 ) ) ;
#9583=AXIS2_PLACEMENT_3D ( 'NONE', #48943, #38736, #7375 ) ;
#9588=EDGE_LOOP ( 'NONE', ( #23197, #17596, #12046 ) ) ;
#9681=CARTESIAN_POINT ( 'NONE',  ( 0.000000000000000000, -2.500000000000000000, 0.000000000000000000 ) ) ;
#9771=CARTESIAN_POINT ( 'NONE',  ( 3.542752237027634976, 1.835478060177116566, -9.000000000000007105 ) ) ;
#9809=CARTESIAN_POINT ( 'NONE',  ( -8.252730563585672030, 2.464278740834326520, 3.705851362693083573 ) ) ;
#9824=AXIS2_PLACEMENT_3D ( 'NONE', #53131, #36286, #4917 ) ;
#9843=CARTESIAN_POINT ( 'NONE',  ( -8.920833891111501046, -2.231456886122025640, 2.548662454712524283 ) ) ;
#9852=CARTESIAN_POINT ( 'NONE',  ( 8.690363669209105524, 2.361802048420730493, 2.947848588679143234 ) ) ;
#9953=CARTESIAN_POINT ( 'NONE',  ( 0.000000000000000000, 1.999999999999998668, 0.000000000000000000 ) ) ;
#9960=CARTESIAN_POINT ( 'NONE',  ( -1.502314598737159031E-15, 2.500000000000000000, -9.000000000000000000 ) ) ;
#9970=DIRECTION ( 'NONE',  ( 0.000000000000000000, -1.000000000000000000, 0.000000000000000000 ) ) ;
#10025=DIRECTION ( 'NONE',  ( 0.000000000000000000, 0.000000000000000000, 1.000000000000000000 ) ) ;
#10086=DIRECTION ( 'NONE',  ( 0.000000000000000000, 0.000000000000000000, 1.000000000000000000 ) ) ;
#10138=DIRECTION ( 'NONE',  ( -0.8660254037844385966, 0.000000000000000000, 0.5000000000000003331 ) ) ;
#10317=CARTESIAN_POINT ( 'NONE',  ( 0.000000000000000000, 2.500000000000000000, 0.000000000000000000 ) ) ;
#10337=ORIENTED_EDGE ( 'NONE', *, *, #7612, .T. ) ;
#10435=AXIS2_PLACEMENT_3D ( 'NONE', #9953, #41290, #42357 ) ;
#10463=PRESENTATION_STYLE_ASSIGNMENT (( #59299 ) ) ;
#10469=CARTESIAN_POINT ( 'NONE',  ( 7.566679973970428463, 2.499999999999998224, 4.894125840469273570 ) ) ;
#10545=CARTESIAN_POINT ( 'NONE',  ( -4.390521455347703217, 1.510510638266201910, 9.000000000000001776 ) ) ;
#10602=AXIS2_PLACEMENT_3D ( 'NONE', #31518, #58610, #52999 ) ;
#10700=B_SPLINE_CURVE_WITH_KNOTS ( 'NONE', 3,
 ( #58005, #31936, #63606, #59339, #31226, #31582, #64291, #16498, #53065, #25954 ),
 .UNSPECIFIED., .F., .F.,
 ( 4, 2, 2, 2, 4 ),
 ( 0.009262909725840906203, 0.01194559479670475113, 0.01328693733213667447, 0.01395760859985263613, 0.01462827986756859780 ),
 .UNSPECIFIED. ) ;
#10732=CARTESIAN_POINT ( 'NONE',  ( -9.985360875542991010, 1.514639124457108244, -0.7048476316491002480 ) ) ;
#10805=ADVANCED_FACE ( 'NONE', ( #58216 ), #2172, .T. ) ;
#10811=CARTESIAN_POINT ( 'NONE',  ( 5.196152422706631135, 1.107695154586740394, 9.000000000000001776 ) ) ;
#10856=( GEOMETRIC_REPRESENTATION_CONTEXT ( 3 ) GLOBAL_UNCERTAINTY_ASSIGNED_CONTEXT ( ( #48309 ) ) GLOBAL_UNIT_ASSIGNED_CONTEXT ( ( #47805, #31894, #16107 ) ) REPRESENTATION_CONTEXT ( 'NONE', 'WORKASPACE' ) );
#10893=EDGE_LOOP ( 'NONE', ( #61757, #37618, #2702 ) ) ;
#11118=ORIENTED_EDGE ( 'NONE', *, *, #22651, .F. ) ;
#11392=CARTESIAN_POINT ( 'NONE',  ( 5.196152422706631135, -1.107695154586740394, 9.000000000000001776 ) ) ;
#11470=EDGE_LOOP ( 'NONE', ( #67175, #55646, #36392 ) ) ;
#11527=EDGE_CURVE ( 'NONE', #47282, #35271, #57478, .T. ) ;
#11580=CARTESIAN_POINT ( 'NONE',  ( -7.794228634059947147, -2.500000000000000000, -4.500000000000000000 ) ) ;
#11584=AXIS2_PLACEMENT_3D ( 'NONE', #31996, #37330, #43314 ) ;
#11613=B_SPLINE_CURVE_WITH_KNOTS ( 'NONE', 3,
 ( #21299, #42469, #58255, #26898, #129, #53343 ),
 .UNSPECIFIED., .F., .F.,
 ( 4, 2, 4 ),
 ( 0.005386537104126977275, 0.008060814333094816833, 0.01073509156206265552 ),
 .UNSPECIFIED. ) ;
#11741=EDGE_CURVE ( 'NONE', #36619, #52251, #44019, .T. ) ;
#11759=ORIENTED_EDGE ( 'NONE', *, *, #43657, .F. ) ;
#11876=CARTESIAN_POINT ( 'NONE',  ( 0.000000000000000000, -2.500000000000000000, 0.000000000000000000 ) ) ;
#11890=DIRECTION ( 'NONE',  ( 0.000000000000000000, 1.000000000000000000, 0.000000000000000000 ) ) ;
#12046=ORIENTED_EDGE ( 'NONE', *, *, #6761, .F. ) ;
#12220=EDGE_CURVE ( 'NONE', #59162, #8712, #64580, .T. ) ;
#12226=ORIENTED_EDGE ( 'NONE', *, *, #63462, .T. ) ;
#12422=CARTESIAN_POINT ( 'NONE',  ( 0.000000000000000000, -2.500000000000000000, 0.000000000000000000 ) ) ;
#12477=PRODUCT_CONTEXT ( 'NONE', #47872, 'mechanical' ) ;
#12525=B_SPLINE_CURVE_WITH_KNOTS ( 'NONE', 3,
 ( #41878, #63296, #30926, #9843, #30216, #69274, #53100, #56975 ),
 .UNSPECIFIED., .F., .F.,
 ( 4, 2, 2, 4 ),
 ( 2.544313220892954975E-07, 0.002693395767724533589, 0.004039966435925755432, 0.005386537104126977275 ),
 .UNSPECIFIED. ) ;
#12574=CARTESIAN_POINT ( 'NONE',  ( 0.000000000000000000, 2.500000000000000000, 9.000000000000001776 ) ) ;
#12640=EDGE_CURVE ( 'NONE', #53362, #16904, #62056, .T. ) ;
#12688=AXIS2_PLACEMENT_3D ( 'NONE', #54388, #6529, #6210 ) ;
#12828=ADVANCED_BREP_SHAPE_REPRESENTATION ( '', ( #3235, #42840 ), #37166 ) ;
#12854=DIRECTION ( 'NONE',  ( 0.000000000000000000, 0.000000000000000000, 1.000000000000000000 ) ) ;
#12894=ORIENTED_EDGE ( 'NONE', *, *, #3209, .F. ) ;
#12947=CARTESIAN_POINT ( 'NONE',  ( -10.39230484541326938, -1.107695154586735509, -1.661048719643172847E-15 ) ) ;
#12962=DIRECTION ( 'NONE',  ( -0.5000000000000002220, 0.000000000000000000, 0.8660254037844384856 ) ) ;
#12993=FACE_OUTER_BOUND ( 'NONE', #59466, .T. ) ;
#13083=( NAMED_UNIT ( * ) SI_UNIT ( $, .STERADIAN. ) SOLID_ANGLE_UNIT ( ) );
#13401=ORIENTED_EDGE ( 'NONE', *, *, #64162, .F. ) ;
#13435=VECTOR ( 'NONE', #57856, 1000.000000000000000 ) ;
#13440=CARTESIAN_POINT ( 'NONE',  ( 0.000000000000000000, -1.999999999999995337, 5.000000000000000000 ) ) ;
#13621=VERTEX_POINT ( 'NONE', #25968 ) ;
#13647=ORIENTED_EDGE ( 'NONE', *, *, #3209, .T. ) ;
#13673=CARTESIAN_POINT ( 'NONE',  ( -9.568252947146932641, 1.861307952554190237, 1.427299755870870435 ) ) ;
#13850=CARTESIAN_POINT ( 'NONE',  ( 7.794228634059945371, 2.500000000000000000, 4.500000000000000888 ) ) ;
#13985=EDGE_CURVE ( 'NONE', #56915, #67877, #11613, .T. ) ;
#14030=CARTESIAN_POINT ( 'NONE',  ( -8.021777294149472937, 2.499999999999994227, 4.105874159530730871 ) ) ;
#14309=VECTOR ( 'NONE', #36182, 1000.000000000000114 ) ;
#14480=ORIENTED_EDGE ( 'NONE', *, *, #45154, .F. ) ;
#14600=CARTESIAN_POINT ( 'NONE',  ( 4.383776131304275125, -1.496531397472843361, -9.000000000000007105 ) ) ;
#14733=CARTESIAN_POINT ( 'NONE',  ( -8.701243704650556410, 2.329718218673040298, 2.929003814506404790 ) ) ;
#14759=PRODUCT_DEFINITION_SHAPE ( 'NONE', 'NONE',  #32611 ) ;
#14847=CARTESIAN_POINT ( 'NONE',  ( 5.196152422706628471, 2.500000000000000000, -9.000000000000005329 ) ) ;
#15064=CARTESIAN_POINT ( 'NONE',  ( 4.793834890952473948, 1.308853920463818987, -9.000000000000007105 ) ) ;
#15075=EDGE_LOOP ( 'NONE', ( #56277, #3463, #49011 ) ) ;
#15222=CARTESIAN_POINT ( 'NONE',  ( 0.000000000000000000, 2.500000000000000000, 0.000000000000000000 ) ) ;
#15281=ORIENTED_EDGE ( 'NONE', *, *, #33593, .F. ) ;
#15303=ADVANCED_FACE ( 'NONE', ( #29950 ), #35939, .F. ) ;
#15327=ORIENTED_EDGE ( 'NONE', *, *, #60829, .F. ) ;
#15423=EDGE_LOOP ( 'NONE', ( #7336, #60424, #36272 ) ) ;
#15459=CONICAL_SURFACE ( 'NONE', #9824, 9.000000000000000000, 0.7853981633974500554 ) ;
#15489=CARTESIAN_POINT ( 'NONE',  ( 9.985360875542987458, 1.514639124457112018, 0.7048476316490990268 ) ) ;
#15587=FACE_OUTER_BOUND ( 'NONE', #38878, .T. ) ;
#15606=DIRECTION ( 'NONE',  ( 0.000000000000000000, 0.000000000000000000, 1.000000000000000000 ) ) ;
#16079=CLOSED_SHELL ( 'NONE', ( #26654, #23825, #6136, #64670, #8263, #52437, #63621, #15303, #3444, #25835, #52392, #38332, #55285, #62385, #25634, #56743, #3801, #7149, #31830, #48965, #10805, #59840, #30226, #62030, #69158, #26658 ) ) ;
#16098=LINE ( 'NONE', #26923, #50701 ) ;
#16107=( NAMED_UNIT ( * ) SI_UNIT ( $, .STERADIAN. ) SOLID_ANGLE_UNIT ( ) );
#16370=CARTESIAN_POINT ( 'NONE',  ( 3.109477999331723641, -1.987149502472171703, 9.000000000000001776 ) ) ;
#16468=VECTOR ( 'NONE', #56545, 1000.000000000000000 ) ;
#16498=CARTESIAN_POINT ( 'NONE',  ( -0.4575609230677321060, -2.491211107078691089, 9.000000000000003553 ) ) ;
#16613=CARTESIAN_POINT ( 'NONE',  ( -4.390521455347699664, 1.510510638266201466, -9.000000000000003553 ) ) ;
#16904=VERTEX_POINT ( 'NONE', #26242 ) ;
#17048=DIRECTION ( 'NONE',  ( 0.000000000000000000, -1.000000000000000000, 0.000000000000000000 ) ) ;
#17149=CARTESIAN_POINT ( 'NONE',  ( 6.021969435454494146, 1.863712308906143589, -7.569642976165943615 ) ) ;
#17168=ORIENTED_EDGE ( 'NONE', *, *, #23555, .T. ) ;
#17169=DIRECTION ( 'NONE',  ( 0.000000000000000000, 0.000000000000000000, 1.000000000000000000 ) ) ;
#17268=CARTESIAN_POINT ( 'NONE',  ( 5.196152422706628471, 1.107695154586738173, -9.000000000000005329 ) ) ;
#17273=CARTESIAN_POINT ( 'NONE',  ( -5.603568002170373319, 1.515110734050471919, -8.294335516573692502 ) ) ;
#17596=ORIENTED_EDGE ( 'NONE', *, *, #61532, .F. ) ;
#17629=CARTESIAN_POINT ( 'NONE',  ( 0.000000000000000000, 2.500000000000000000, 0.000000000000000000 ) ) ;
#17630=CARTESIAN_POINT ( 'NONE',  ( 0.000000000000000000, 1.999999999999998668, 5.000000000000000000 ) ) ;
#17682=AXIS2_PLACEMENT_3D ( 'NONE', #44070, #33131, #7757 ) ;
#17844=ORIENTED_EDGE ( 'NONE', *, *, #40846, .T. ) ;
#17858=FACE_OUTER_BOUND ( 'NONE', #58666, .T. ) ;
#17995=ORIENTED_EDGE ( 'NONE', *, *, #41413, .F. ) ;
#18257=VECTOR ( 'NONE', #62078, 1000.000000000000114 ) ;
#18297=VERTEX_POINT ( 'NONE', #64103 ) ;
#18474=PRODUCT_DEFINITION_CONTEXT ( 'detailed design', #21288, 'design' ) ;
#18484=ORIENTED_EDGE ( 'NONE', *, *, #22651, .T. ) ;
#18721=CARTESIAN_POINT ( 'NONE',  ( 0.000000000000000000, -2.500000000000000000, 9.000000000000000000 ) ) ;
#18771=ORIENTED_EDGE ( 'NONE', *, *, #11527, .T. ) ;
#19093=ORIENTED_EDGE ( 'NONE', *, *, #60685, .T. ) ;
#19104=AXIS2_PLACEMENT_3D ( 'NONE', #15222, #41958, #28027 ) ;
#19122=MECHANICAL_DESIGN_GEOMETRIC_PRESENTATION_REPRESENTATION('',(#43888),#61786);
#19204=CARTESIAN_POINT ( 'NONE',  ( 9.568252947146927312, -1.861307952554195566, -1.427299755870872433 ) ) ;
#19219=CARTESIAN_POINT ( 'NONE',  ( 0.000000000000000000, 2.500000000000000000, 9.000000000000001776 ) ) ;
#19244=EDGE_LOOP ( 'NONE', ( #49834, #19456, #51765, #29443 ) ) ;
#19271=ORIENTED_EDGE ( 'NONE', *, *, #62164, .F. ) ;
#19275=EDGE_CURVE ( 'NONE', #16904, #51850, #34380, .T. ) ;
#19424=EDGE_LOOP ( 'NONE', ( #19271, #41037, #15327 ) ) ;
#19456=ORIENTED_EDGE ( 'NONE', *, *, #29275, .T. ) ;
#19518=CARTESIAN_POINT ( 'NONE',  ( 0.000000000000000000, -2.500000000000000000, 5.000000000000000000 ) ) ;
#19608=ORIENTED_EDGE ( 'NONE', *, *, #41413, .T. ) ;
#19649=AXIS2_PLACEMENT_3D ( 'NONE', #65198, #17048, #10025 ) ;
#19728=ORIENTED_EDGE ( 'NONE', *, *, #38026, .T. ) ;
#19869=CARTESIAN_POINT ( 'NONE',  ( -5.196152422706636465, -1.107695154586736175, -9.000000000000003553 ) ) ;
#19876=DIRECTION ( 'NONE',  ( 0.000000000000000000, 1.000000000000000000, 0.000000000000000000 ) ) ;
#19927=CARTESIAN_POINT ( 'NONE',  ( -5.196152422706636465, -1.107695154586736175, -9.000000000000003553 ) ) ;
#20048=ORIENTED_EDGE ( 'NONE', *, *, #45575, .T. ) ;
#20187=FACE_OUTER_BOUND ( 'NONE', #64015, .T. ) ;
#20287=VERTEX_POINT ( 'NONE', #57917 ) ;
#20460=CIRCLE ( 'NONE', #31701, 5.000000000000000000 ) ;
#20553=CARTESIAN_POINT ( 'NONE',  ( 5.196152422706631135, -1.107695154586740394, 9.000000000000001776 ) ) ;
#20638=CARTESIAN_POINT ( 'NONE',  ( -0.4575609230677349926, -2.491211107078686648, -9.000000000000003553 ) ) ;
#20925=CARTESIAN_POINT ( 'NONE',  ( 3.109477999331718312, -1.987149502472170370, -9.000000000000005329 ) ) ;
#20943=CARTESIAN_POINT ( 'NONE',  ( -9.566487832665403701, 1.863712308906138704, -1.430357023834059271 ) ) ;
#20961=MECHANICAL_DESIGN_GEOMETRIC_PRESENTATION_REPRESENTATION('',(#23220),#10856);
#21103=CARTESIAN_POINT ( 'NONE',  ( -6.667623377008405683, -2.231456886122025196, -6.451337545287480602 ) ) ;
#21170=CIRCLE ( 'NONE', #39183, 9.000000000000000000 ) ;
#21173=EDGE_LOOP ( 'NONE', ( #54125, #3947, #55431 ) ) ;
#21242=CARTESIAN_POINT ( 'NONE',  ( 0.000000000000000000, -2.500000000000000000, 9.000000000000000000 ) ) ;
#21254=CARTESIAN_POINT ( 'NONE',  ( -7.794228634059947147, 2.500000000000000000, -4.500000000000000000 ) ) ;
#21288=APPLICATION_CONTEXT ( 'automotive_design' ) ;
#21299=CARTESIAN_POINT ( 'NONE',  ( -7.794228634059948035, -2.500000000000000000, 4.499999999999999112 ) ) ;
#21531=ORIENTED_EDGE ( 'NONE', *, *, #45154, .T. ) ;
#21556=DIRECTION ( 'NONE',  ( -0.000000000000000000, -1.000000000000000000, -0.000000000000000000 ) ) ;
#21754=CARTESIAN_POINT ( 'NONE',  ( -10.39230484541326938, 1.107695154586735509, -1.661048719744147042E-15 ) ) ;
#21854=ORIENTED_EDGE ( 'NONE', *, *, #11741, .T. ) ;
#21866=AXIS2_PLACEMENT_3D ( 'NONE', #3510, #25014, #62631 ) ;
#21867=ORIENTED_EDGE ( 'NONE', *, *, #42162, .T. ) ;
#22075=FACE_OUTER_BOUND ( 'NONE', #28007, .T. ) ;
#22091=DIRECTION ( 'NONE',  ( 0.000000000000000000, 0.000000000000000000, 1.000000000000000000 ) ) ;
#22144=CARTESIAN_POINT ( 'NONE',  ( -5.603568002170373319, -1.515110734050471919, -8.294335516573692502 ) ) ;
#22209=DIRECTION ( 'NONE',  ( 0.000000000000000000, 1.000000000000000000, 0.000000000000000000 ) ) ;
#22316=VERTEX_POINT ( 'NONE', #52335 ) ;
#22448=AXIS2_PLACEMENT_3D ( 'NONE', #9208, #30627, #52133 ) ;
#22518=CARTESIAN_POINT ( 'NONE',  ( -7.335726704534230258, 2.464278740834323411, -5.294148637306920868 ) ) ;
#22619=CARTESIAN_POINT ( 'NONE',  ( 10.39230484541326582, -1.107695154586738839, 1.440973567693753677E-18 ) ) ;
#22651=EDGE_CURVE ( 'NONE', #33880, #39293, #50853, .T. ) ;
#22797=CONICAL_SURFACE ( 'NONE', #12688, 9.000000000000000000, 0.7853981633974500554 ) ;
#22980=FACE_OUTER_BOUND ( 'NONE', #64641, .T. ) ;
#23197=ORIENTED_EDGE ( 'NONE', *, *, #69263, .F. ) ;
#23220=STYLED_ITEM ( 'NONE', ( #10463 ), #3235 ) ;
#23252=CARTESIAN_POINT ( 'NONE',  ( 0.000000000000000000, -1.999999999999995337, 0.000000000000000000 ) ) ;
#23327=CARTESIAN_POINT ( 'NONE',  ( 0.000000000000000000, -2.500000000000000000, -5.500000000000005329 ) ) ;
#23451=CARTESIAN_POINT ( 'NONE',  ( 9.984889265949528081, -1.515110734050476582, -0.7056644834263100519 ) ) ;
#23555=EDGE_CURVE ( 'NONE', #33880, #47282, #67371, .T. ) ;
#23616=VERTEX_POINT ( 'NONE', #19869 ) ;
#23825=ADVANCED_FACE ( 'NONE', ( #56753 ), #31752, .F. ) ;
#23904=CONICAL_SURFACE ( 'NONE', #37430, 9.000000000000000000, 0.7853981633974500554 ) ;
#24091=CARTESIAN_POINT ( 'NONE',  ( 6.735557395310443995E-16, 2.500000000000000000, -5.500000000000001776 ) ) ;
#24197=VECTOR ( 'NONE', #47598, 1000.000000000000000 ) ;
#24418=EDGE_CURVE ( 'NONE', #16904, #22316, #40717, .T. ) ;
#24589=CARTESIAN_POINT ( 'NONE',  ( 0.000000000000000000, 2.500000000000000000, 0.000000000000000000 ) ) ;
#24751=EDGE_CURVE ( 'NONE', #66441, #53362, #69693, .T. ) ;
#24764=CARTESIAN_POINT ( 'NONE',  ( -5.196152422706636465, 2.500000000000000000, 9.000000000000001776 ) ) ;
#24772=ORIENTED_EDGE ( 'NONE', *, *, #46692, .F. ) ;
#24783=CARTESIAN_POINT ( 'NONE',  ( 0.000000000000000000, -2.500000000000000000, 0.000000000000000000 ) ) ;
#25014=DIRECTION ( 'NONE',  ( -0.000000000000000000, -1.000000000000000000, -0.000000000000000000 ) ) ;
#25136=ORIENTED_EDGE ( 'NONE', *, *, #39007, .T. ) ;
#25243=CARTESIAN_POINT ( 'NONE',  ( 6.887213563469345878, 2.329718218673042962, 6.070996185493596542 ) ) ;
#25276=ORIENTED_EDGE ( 'NONE', *, *, #29472, .T. ) ;
#25292=ORIENTED_EDGE ( 'NONE', *, *, #27840, .T. ) ;
#25376=( NAMED_UNIT ( * ) PLANE_ANGLE_UNIT ( ) SI_UNIT ( $, .RADIAN. ) );
#25486=CARTESIAN_POINT ( 'NONE',  ( 3.542752237027634976, -1.835478060177116566, -9.000000000000007105 ) ) ;
#25599=CARTESIAN_POINT ( 'NONE',  ( -7.794228634059948035, 2.500000000000000000, 4.499999999999999112 ) ) ;
#25634=ADVANCED_FACE ( 'NONE', ( #4667 ), #32849, .T. ) ;
#25721=EDGE_CURVE ( 'NONE', #33218, #28673, #33942, .T. ) ;
#25835=ADVANCED_FACE ( 'NONE', ( #5692 ), #23904, .T. ) ;
#25897=ORIENTED_EDGE ( 'NONE', *, *, #6761, .T. ) ;
#25939=EDGE_LOOP ( 'NONE', ( #14480, #46565, #1899, #54616, #48717, #36897 ) ) ;
#25954=CARTESIAN_POINT ( 'NONE',  ( 0.000000000000000000, -2.500000000000000000, 9.000000000000000000 ) ) ;
#25968=CARTESIAN_POINT ( 'NONE',  ( -7.794228634059947147, -2.500000000000000000, -4.500000000000000000 ) ) ;
#26120=DIRECTION ( 'NONE',  ( 0.000000000000000000, 1.000000000000000000, 0.000000000000000000 ) ) ;
#26166=CARTESIAN_POINT ( 'NONE',  ( 7.335726704534224041, -2.464278740834329184, 5.294148637306918204 ) ) ;
#26198=ORIENTED_EDGE ( 'NONE', *, *, #49490, .T. ) ;
#26242=CARTESIAN_POINT ( 'NONE',  ( 7.794228634059946259, -2.500000000000000000, -4.500000000000001776 ) ) ;
#26257=EDGE_LOOP ( 'NONE', ( #48555, #38111, #25292, #57531, #54889, #24772 ) ) ;
#26264=CARTESIAN_POINT ( 'NONE',  ( 1.802043943559349604, 2.359472279213374435, -9.000000000000007105 ) ) ;
#26408=AXIS2_PLACEMENT_3D ( 'NONE', #57631, #10138, #4128 ) ;
#26437=AXIS2_PLACEMENT_3D ( 'NONE', #678, #22209, #47619 ) ;
#26453=EDGE_CURVE ( 'NONE', #53612, #45556, #39682, .T. ) ;
#26506=AXIS2_PLACEMENT_3D ( 'NONE', #52004, #8732, #12962 ) ;
#26574=CARTESIAN_POINT ( 'NONE',  ( 5.196152422706628471, -1.107695154586738173, -9.000000000000005329 ) ) ;
#26631=CARTESIAN_POINT ( 'NONE',  ( 0.000000000000000000, 2.500000000000000000, 0.000000000000000000 ) ) ;
#26654=ADVANCED_FACE ( 'NONE', ( #6236 ), #64432, .F. ) ;
#26658=ADVANCED_FACE ( 'NONE', ( #22075 ), #54328, .F. ) ;
#26682=CARTESIAN_POINT ( 'NONE',  ( -1.804616585955809649, 2.331456807317426438, 9.000000000000000000 ) ) ;
#26784=CARTESIAN_POINT ( 'NONE',  ( 7.794228634059945371, -2.500000000000000000, 4.500000000000000888 ) ) ;
#26790=DIRECTION ( 'NONE',  ( 0.000000000000000000, -1.000000000000000000, 0.000000000000000000 ) ) ;
#26898=CARTESIAN_POINT ( 'NONE',  ( -6.021969435454500363, -1.863712308906140258, 7.569642976165947168 ) ) ;
#26923=CARTESIAN_POINT ( 'NONE',  ( 6.123233995736766282E-16, -2.500000000000000000, -5.000000000000000000 ) ) ;
#26938=CIRCLE ( 'NONE', #5616, 9.000000000000000000 ) ;
#27010=DIRECTION ( 'NONE',  ( 0.000000000000000000, 1.000000000000000000, 0.000000000000000000 ) ) ;
#27199=CARTESIAN_POINT ( 'NONE',  ( 4.383776131304280455, -1.496531397472844693, 9.000000000000003553 ) ) ;
#27319=DIRECTION ( 'NONE',  ( 0.000000000000000000, 0.000000000000000000, 1.000000000000000000 ) ) ;
#27349=CARTESIAN_POINT ( 'NONE',  ( 0.000000000000000000, 1.999999999999998668, 0.000000000000000000 ) ) ;
#27461=CARTESIAN_POINT ( 'NONE',  ( -1.502314598737159031E-15, 2.500000000000000000, -9.000000000000000000 ) ) ;
#27462=FACE_OUTER_BOUND ( 'NONE', #3626, .T. ) ;
#27750=FACE_OUTER_BOUND ( 'NONE', #28805, .T. ) ;
#27794=CARTESIAN_POINT ( 'NONE',  ( -0.2278693232858696738, 2.499999999999995115, -9.000000000000007105 ) ) ;
#27833=ORIENTED_EDGE ( 'NONE', *, *, #58769, .F. ) ;
#27840=EDGE_CURVE ( 'NONE', #22316, #53362, #44685, .T. ) ;
#28007=EDGE_LOOP ( 'NONE', ( #3732, #36176, #35900, #39350 ) ) ;
#28027=DIRECTION ( 'NONE',  ( 0.000000000000000000, 0.000000000000000000, 1.000000000000000000 ) ) ;
#28331=CARTESIAN_POINT ( 'NONE',  ( 5.603096392576905949, 1.514639124457112240, -8.295152368350905192 ) ) ;
#28388=CARTESIAN_POINT ( 'NONE',  ( 4.793834890952475725, 1.308853920463818987, 9.000000000000005329 ) ) ;
#28443=ORIENTED_EDGE ( 'NONE', *, *, #39007, .F. ) ;
#28444=AXIS2_PLACEMENT_3D ( 'NONE', #4851, #69562, #548 ) ;
#28557=CONICAL_SURFACE ( 'NONE', #52220, 9.000000000000000000, 0.7853981633974500554 ) ;
#28649=CARTESIAN_POINT ( 'NONE',  ( 5.196152422706631135, 2.500000000000000000, 9.000000000000001776 ) ) ;
#28673=VERTEX_POINT ( 'NONE', #13850 ) ;
#28708=CARTESIAN_POINT ( 'NONE',  ( 6.898093598910793212, -2.361802048420730049, -6.052151411320861207 ) ) ;
#28805=EDGE_LOOP ( 'NONE', ( #25136, #10337, #25897, #12894, #66697, #48738 ) ) ;
#28918=ORIENTED_EDGE ( 'NONE', *, *, #30975, .T. ) ;
#29066=CARTESIAN_POINT ( 'NONE',  ( 0.000000000000000000, -2.500000000000000000, 0.000000000000000000 ) ) ;
#29068=CARTESIAN_POINT ( 'NONE',  ( 8.920833891111493941, 2.231456886122029193, -2.548662454712524728 ) ) ;
#29086=VERTEX_POINT ( 'NONE', #17268 ) ;
#29275=EDGE_CURVE ( 'NONE', #36711, #52251, #44361, .T. ) ;
#29408=CARTESIAN_POINT ( 'NONE',  ( 5.603096392576905949, -1.514639124457112240, -8.295152368350905192 ) ) ;
#29437=CARTESIAN_POINT ( 'NONE',  ( 7.794228634059946259, 2.500000000000000000, -4.500000000000001776 ) ) ;
#29443=ORIENTED_EDGE ( 'NONE', *, *, #40846, .F. ) ;
#29472=EDGE_CURVE ( 'NONE', #8712, #45556, #56519, .T. ) ;
#29611=CARTESIAN_POINT ( 'NONE',  ( -5.196152422706636465, -1.107695154586737063, 9.000000000000001776 ) ) ;
#29616=SHAPE_REPRESENTATION_RELATIONSHIP ( 'NONE' , 'NONE' ,  #38844, #12828 ) ;
#29734=DIRECTION ( 'NONE',  ( 1.776356839400250465E-15, 0.000000000000000000, 1.000000000000000000 ) ) ;
#29950=FACE_OUTER_BOUND ( 'NONE', #63491, .T. ) ;
#30046=ORIENTED_EDGE ( 'NONE', *, *, #40080, .F. ) ;
#30211=FACE_OUTER_BOUND ( 'NONE', #15075, .T. ) ;
#30216=CARTESIAN_POINT ( 'NONE',  ( -8.701243704650556410, -2.329718218673039853, 2.929003814506404790 ) ) ;
#30226=ADVANCED_FACE ( 'NONE', ( #33525, #6436 ), #6781, .F. ) ;
#30428=PRODUCT ( '11. Nut M10', '11. Nut M10', '', ( #12477 ) ) ;
#30627=DIRECTION ( 'NONE',  ( 0.8660254037844387076, 0.000000000000000000, -0.4999999999999999445 ) ) ;
#30748=CARTESIAN_POINT ( 'NONE',  ( 6.667623377008403018, -2.231456886122029193, 6.451337545287477937 ) ) ;
#30797=AXIS2_PLACEMENT_3D ( 'NONE', #24589, #51703, #67176 ) ;
#30876=DIRECTION ( 'NONE',  ( 0.000000000000000000, 1.000000000000000000, 0.000000000000000000 ) ) ;
#30926=CARTESIAN_POINT ( 'NONE',  ( -9.568252947146932641, -1.861307952554191347, 1.427299755870870435 ) ) ;
#30934=ORIENTED_EDGE ( 'NONE', *, *, #49266, .T. ) ;
#30975=EDGE_CURVE ( 'NONE', #33218, #4344, #64568, .T. ) ;
#31226=CARTESIAN_POINT ( 'NONE',  ( -1.804616585955809649, -2.331456807317426438, 9.000000000000000000 ) ) ;
#31229=DIRECTION ( 'NONE',  ( -0.000000000000000000, -1.000000000000000000, -0.000000000000000000 ) ) ;
#31513=AXIS2_PLACEMENT_3D ( 'NONE', #60930, #38147, #49054 ) ;
#31518=CARTESIAN_POINT ( 'NONE',  ( 0.000000000000000000, -2.500000000000000000, 0.000000000000000000 ) ) ;
#31532=CARTESIAN_POINT ( 'NONE',  ( 0.000000000000000000, -1.999999999999995337, 0.000000000000000000 ) ) ;
#31582=CARTESIAN_POINT ( 'NONE',  ( -1.135663242406173001, -2.431311185535292907, 9.000000000000003553 ) ) ;
#31651=FACE_OUTER_BOUND ( 'NONE', #51196, .T. ) ;
#31701=AXIS2_PLACEMENT_3D ( 'NONE', #27349, #11890, #5550 ) ;
#31743=CARTESIAN_POINT ( 'NONE',  ( 0.000000000000000000, 2.500000000000000000, 0.000000000000000000 ) ) ;
#31752=CONICAL_SURFACE ( 'NONE', #10435, 5.000000000000000000, 0.7853981633974482790 ) ;
#31804=CARTESIAN_POINT ( 'NONE',  ( 4.793834890952473948, -1.308853920463818987, -9.000000000000007105 ) ) ;
#31830=ADVANCED_FACE ( 'NONE', ( #64661 ), #36546, .T. ) ;
#31894=( NAMED_UNIT ( * ) PLANE_ANGLE_UNIT ( ) SI_UNIT ( $, .RADIAN. ) );
#31936=CARTESIAN_POINT ( 'NONE',  ( -4.390521455347703217, -1.510510638266201910, 9.000000000000001776 ) ) ;
#31972=DIRECTION ( 'NONE',  ( 0.000000000000000000, 0.000000000000000000, 1.000000000000000000 ) ) ;
#31984=CARTESIAN_POINT ( 'NONE',  ( -3.542344102440326825, 1.863645424029198194, 9.000000000000000000 ) ) ;
#31996=CARTESIAN_POINT ( 'NONE',  ( 0.000000000000000000, 2.500000000000000000, 0.000000000000000000 ) ) ;
#32182=EDGE_LOOP ( 'NONE', ( #18484, #20048, #19093, #52878 ) ) ;
#32259=CARTESIAN_POINT ( 'NONE',  ( 6.123233995736766282E-16, 1.999999999999998668, -5.000000000000000000 ) ) ;
#32341=CARTESIAN_POINT ( 'NONE',  ( -6.020204320972970535, -1.861307952554190903, -7.572700244129129565 ) ) ;
#32611=PRODUCT_DEFINITION ( 'UNKNOWN', '', #36031, #18474 ) ;
#32849=CONICAL_SURFACE ( 'NONE', #2403, 9.000000000000000000, 0.7853981633974500554 ) ;
#32900=VECTOR ( 'NONE', #40434, 1000.000000000000114 ) ;
#32954=FACE_OUTER_BOUND ( 'NONE', #11470, .T. ) ;
#33123=EDGE_CURVE ( 'NONE', #47020, #8712, #49465, .T. ) ;
#33131=DIRECTION ( 'NONE',  ( 0.000000000000000000, 1.000000000000000000, 0.000000000000000000 ) ) ;
#33155=CARTESIAN_POINT ( 'NONE',  ( -6.898093598910797652, 2.361802048420727385, 6.052151411320861207 ) ) ;
#33207=VECTOR ( 'NONE', #40903, 1000.000000000000000 ) ;
#33218=VERTEX_POINT ( 'NONE', #19219 ) ;
#33286=EDGE_CURVE ( 'NONE', #66441, #46816, #45882, .T. ) ;
#33325=DIRECTION ( 'NONE',  ( -0.000000000000000000, -1.000000000000000000, -0.000000000000000000 ) ) ;
#33525=FACE_BOUND ( 'NONE', #64871, .T. ) ;
#33593=EDGE_CURVE ( 'NONE', #20287, #67877, #63112, .T. ) ;
#33637=CARTESIAN_POINT ( 'NONE',  ( 6.898093598910793212, 2.361802048420730049, -6.052151411320861207 ) ) ;
#33692=CARTESIAN_POINT ( 'NONE',  ( 0.9126302363882010660, 2.499999999999998224, 9.000000000000003553 ) ) ;
#33854=CARTESIAN_POINT ( 'NONE',  ( 5.196152422706628471, 2.500000000000000000, -9.000000000000005329 ) ) ;
#33880=VERTEX_POINT ( 'NONE', #13440 ) ;
#33914=CARTESIAN_POINT ( 'NONE',  ( 10.39230484541326582, 1.107695154586738839, 1.440973567693753677E-18 ) ) ;
#33942=CIRCLE ( 'NONE', #50780, 9.000000000000000000 ) ;
#34046=ORIENTED_EDGE ( 'NONE', *, *, #46692, .T. ) ;
#34121=DIRECTION ( 'NONE',  ( 0.000000000000000000, 1.000000000000000000, 0.000000000000000000 ) ) ;
#34380=B_SPLINE_CURVE_WITH_KNOTS ( 'NONE', 3,
 ( #55093, #49853, #28708, #50196, #29408, #2639 ),
 .UNSPECIFIED., .F., .F.,
 ( 4, 2, 4 ),
 ( 0.005386537104126977275, 0.008060814333094818568, 0.01073509156206266073 ),
 .UNSPECIFIED. ) ;
#34840=CARTESIAN_POINT ( 'NONE',  ( 0.000000000000000000, 1.999999999999998668, 5.000000000000000000 ) ) ;
#34893=FILL_AREA_STYLE_COLOUR ( '', #38263 ) ;
#35018=PLANE ( 'NONE',  #7539 ) ;
#35098=CARTESIAN_POINT ( 'NONE',  ( -10.39230484541326938, 2.500000000000000000, -1.734723475976807094E-15 ) ) ;
#35133=CARTESIAN_POINT ( 'NONE',  ( -9.984889265949528081, 1.515110734050472807, 0.7056644834263087196 ) ) ;
#35271=VERTEX_POINT ( 'NONE', #23327 ) ;
#35602=ORIENTED_EDGE ( 'NONE', *, *, #54671, .T. ) ;
#35792=ORIENTED_EDGE ( 'NONE', *, *, #54671, .F. ) ;
#35882=CARTESIAN_POINT ( 'NONE',  ( -7.794228634059948035, -2.500000000000000000, 4.499999999999999112 ) ) ;
#35900=ORIENTED_EDGE ( 'NONE', *, *, #58572, .T. ) ;
#35939=PLANE ( 'NONE',  #22448 ) ;
#35958=DIRECTION ( 'NONE',  ( 0.000000000000000000, 0.000000000000000000, 1.000000000000000000 ) ) ;
#36031=PRODUCT_DEFINITION_FORMATION_WITH_SPECIFIED_SOURCE ( 'ANY', '', #30428, .NOT_KNOWN. ) ;
#36094=AXIS2_PLACEMENT_3D ( 'NONE', #29066, #54766, #6579 ) ;
#36176=ORIENTED_EDGE ( 'NONE', *, *, #49266, .F. ) ;
#36182=DIRECTION ( 'NONE',  ( 0.000000000000000000, -0.7071067811865474617, -0.7071067811865474617 ) ) ;
#36197=CARTESIAN_POINT ( 'NONE',  ( 0.000000000000000000, 2.500000000000000000, 0.000000000000000000 ) ) ;
#36272=ORIENTED_EDGE ( 'NONE', *, *, #68284, .F. ) ;
#36286=DIRECTION ( 'NONE',  ( 0.000000000000000000, 1.000000000000000000, 0.000000000000000000 ) ) ;
#36392=ORIENTED_EDGE ( 'NONE', *, *, #27840, .F. ) ;
#36443=CARTESIAN_POINT ( 'NONE',  ( 6.020204320972966094, -1.861307952554195122, 7.572700244129132230 ) ) ;
#36546=CONICAL_SURFACE ( 'NONE', #64575, 9.000000000000000000, 0.7853981633974500554 ) ;
#36547=EDGE_LOOP ( 'NONE', ( #69016, #53693, #44482 ) ) ;
#36577=CARTESIAN_POINT ( 'NONE',  ( -8.920833891111501046, 2.231456886122024752, 2.548662454712524283 ) ) ;
#36589=CARTESIAN_POINT ( 'NONE',  ( 0.000000000000000000, -2.500000000000000000, 0.000000000000000000 ) ) ;
#36619=VERTEX_POINT ( 'NONE', #63910 ) ;
#36711=VERTEX_POINT ( 'NONE', #32259 ) ;
#36769=ORIENTED_EDGE ( 'NONE', *, *, #13985, .T. ) ;
#36897=ORIENTED_EDGE ( 'NONE', *, *, #24418, .T. ) ;
#37166=( GEOMETRIC_REPRESENTATION_CONTEXT ( 3 ) GLOBAL_UNCERTAINTY_ASSIGNED_CONTEXT ( ( #48096 ) ) GLOBAL_UNIT_ASSIGNED_CONTEXT ( ( #3170, #46543, #45825 ) ) REPRESENTATION_CONTEXT ( 'NONE', 'WORKASPACE' ) );
#37199=CARTESIAN_POINT ( 'NONE',  ( 0.000000000000000000, -2.500000000000000000, 0.000000000000000000 ) ) ;
#37236=CARTESIAN_POINT ( 'NONE',  ( 6.667623377008403018, 2.231456886122029193, 6.451337545287477937 ) ) ;
#37317=CARTESIAN_POINT ( 'NONE',  ( -5.196152422706636465, 1.107695154586737063, 9.000000000000001776 ) ) ;
#37330=DIRECTION ( 'NONE',  ( 0.000000000000000000, -1.000000000000000000, 0.000000000000000000 ) ) ;
#37430=AXIS2_PLACEMENT_3D ( 'NONE', #5348, #26790, #1050 ) ;
#37525=CIRCLE ( 'NONE', #7137, 9.000000000000000000 ) ;
#37580=DIRECTION ( 'NONE',  ( -0.000000000000000000, 1.000000000000000000, -0.000000000000000000 ) ) ;
#37618=ORIENTED_EDGE ( 'NONE', *, *, #40080, .T. ) ;
#37682=CONICAL_SURFACE ( 'NONE', #19649, 9.000000000000000000, 0.7853981633974500554 ) ;
#37689=CARTESIAN_POINT ( 'NONE',  ( 6.735557395310448926E-16, -2.500000000000000000, 5.500000000000005329 ) ) ;
#37752=CARTESIAN_POINT ( 'NONE',  ( -5.196152422706636465, 1.107695154586736175, -9.000000000000003553 ) ) ;
#37925=SURFACE_SIDE_STYLE ('',( #5483 ) ) ;
#38026=EDGE_CURVE ( 'NONE', #46816, #47020, #39786, .T. ) ;
#38111=ORIENTED_EDGE ( 'NONE', *, *, #48601, .T. ) ;
#38147=DIRECTION ( 'NONE',  ( 0.000000000000000000, -1.000000000000000000, 0.000000000000000000 ) ) ;
#38263=COLOUR_RGB ( '', 0.66274510, 0.83137255, 0.94901961) ;
#38332=ADVANCED_FACE ( 'NONE', ( #30211 ), #6099, .T. ) ;
#38700=CARTESIAN_POINT ( 'NONE',  ( -7.794228634059947147, -2.500000000000000000, -4.500000000000000000 ) ) ;
#38736=DIRECTION ( 'NONE',  ( 0.8660254037844387076, -0.000000000000000000, 0.5000000000000001110 ) ) ;
#38844=SHAPE_REPRESENTATION ( '11. Nut M10', ( #42840 ), #37166 ) ;
#38878=EDGE_LOOP ( 'NONE', ( #65016, #3204, #35602, #13401, #52586, #69315 ) ) ;
#39007=EDGE_CURVE ( 'NONE', #59162, #23616, #51803, .T. ) ;
#39016=CARTESIAN_POINT ( 'NONE',  ( 3.109477999331723641, 1.987149502472171703, 9.000000000000001776 ) ) ;
#39116=CARTESIAN_POINT ( 'NONE',  ( -1.585182400056157181, 2.380245935246553035, -9.000000000000005329 ) ) ;
#39150=CARTESIAN_POINT ( 'NONE',  ( -5.196152422706636465, 1.107695154586737063, 9.000000000000001776 ) ) ;
#39183=AXIS2_PLACEMENT_3D ( 'NONE', #36197, #30876, #63919 ) ;
#39293=VERTEX_POINT ( 'NONE', #1005 ) ;
#39350=ORIENTED_EDGE ( 'NONE', *, *, #11527, .F. ) ;
#39392=ORIENTED_EDGE ( 'NONE', *, *, #12640, .T. ) ;
#39410=CARTESIAN_POINT ( 'NONE',  ( 6.123233995736766282E-16, 1.999999999999998668, -5.000000000000000000 ) ) ;
#39419=DIRECTION ( 'NONE',  ( 0.000000000000000000, 1.000000000000000000, 0.000000000000000000 ) ) ;
#39432=AXIS2_PLACEMENT_3D ( 'NONE', #4258, #41980, #3928 ) ;
#39487=ORIENTED_EDGE ( 'NONE', *, *, #64346, .F. ) ;
#39538=ORIENTED_EDGE ( 'NONE', *, *, #33123, .T. ) ;
#39682=B_SPLINE_CURVE_WITH_KNOTS ( 'NONE', 3,
 ( #46426, #35133, #13673, #36577, #14733, #9809, #14030, #25599 ),
 .UNSPECIFIED., .F., .F.,
 ( 4, 2, 2, 4 ),
 ( 2.544313220892349347E-07, 0.002693395767724533155, 0.004039966435925755432, 0.005386537104126977275 ),
 .UNSPECIFIED. ) ;
#39767=DIRECTION ( 'NONE',  ( 0.000000000000000000, 0.000000000000000000, 1.000000000000000000 ) ) ;
#39786=CIRCLE ( 'NONE', #49857, 9.000000000000000000 ) ;
#39809=DIRECTION ( 'NONE',  ( 0.000000000000000000, 0.000000000000000000, 1.000000000000000000 ) ) ;
#39970=AXIS2_PLACEMENT_3D ( 'NONE', #31532, #53685, #69518 ) ;
#39979=DIRECTION ( 'NONE',  ( -0.000000000000000000, 1.000000000000000000, -0.000000000000000000 ) ) ;
#40073=CARTESIAN_POINT ( 'NONE',  ( -0.2278693232858663154, 2.499999999999997780, 9.000000000000003553 ) ) ;
#40080=EDGE_CURVE ( 'NONE', #29086, #47020, #42827, .T. ) ;
#40192=SURFACE_STYLE_USAGE ( .BOTH. , #56339 ) ;
#40283=SHAPE_DEFINITION_REPRESENTATION ( #14759, #38844 ) ;
#40411=FACE_OUTER_BOUND ( 'NONE', #26257, .T. ) ;
#40434=DIRECTION ( 'NONE',  ( 8.659560562354932858E-17, 0.7071067811865474617, -0.7071067811865474617 ) ) ;
#40622=EDGE_CURVE ( 'NONE', #35271, #47282, #43517, .T. ) ;
#40717=CIRCLE ( 'NONE', #53048, 9.000000000000000000 ) ;
#40846=EDGE_CURVE ( 'NONE', #60416, #36619, #46131, .T. ) ;
#40878=ORIENTED_EDGE ( 'NONE', *, *, #13985, .F. ) ;
#40903=DIRECTION ( 'NONE',  ( -0.000000000000000000, -1.000000000000000000, -0.000000000000000000 ) ) ;
#41007=CARTESIAN_POINT ( 'NONE',  ( 6.887213563469345878, -2.329718218673042962, 6.070996185493596542 ) ) ;
#41037=ORIENTED_EDGE ( 'NONE', *, *, #7612, .F. ) ;
#41281=FACE_OUTER_BOUND ( 'NONE', #32182, .T. ) ;
#41290=DIRECTION ( 'NONE',  ( 0.000000000000000000, 1.000000000000000000, 0.000000000000000000 ) ) ;
#41413=EDGE_CURVE ( 'NONE', #60416, #36711, #61503, .T. ) ;
#41544=AXIS2_PLACEMENT_3D ( 'NONE', #68790, #19876, #42100 ) ;
#41780=B_SPLINE_CURVE_WITH_KNOTS ( 'NONE', 3,
 ( #21254, #47740, #69137, #20943, #10732, #53633 ),
 .UNSPECIFIED., .F., .F.,
 ( 4, 2, 4 ),
 ( 0.005386537104126974673, 0.008060814333094815098, 0.01073509156206265379 ),
 .UNSPECIFIED. ) ;
#41878=CARTESIAN_POINT ( 'NONE',  ( -10.39230484541326938, -1.107695154586735509, -1.661048719643172847E-15 ) ) ;
#41958=DIRECTION ( 'NONE',  ( 0.000000000000000000, 1.000000000000000000, 0.000000000000000000 ) ) ;
#41980=DIRECTION ( 'NONE',  ( -0.000000000000000000, 1.000000000000000000, -0.000000000000000000 ) ) ;
#41987=EDGE_CURVE ( 'NONE', #45556, #20287, #57871, .T. ) ;
#42100=DIRECTION ( 'NONE',  ( 0.000000000000000000, 0.000000000000000000, 1.000000000000000000 ) ) ;
#42162=EDGE_CURVE ( 'NONE', #28673, #46816, #21170, .T. ) ;
#42357=DIRECTION ( 'NONE',  ( 0.000000000000000000, 0.000000000000000000, 1.000000000000000000 ) ) ;
#42422=CARTESIAN_POINT ( 'NONE',  ( 0.9126302363881977353, -2.499999999999996447, -9.000000000000007105 ) ) ;
#42469=CARTESIAN_POINT ( 'NONE',  ( -7.342319042881618962, -2.499999999999994671, 5.282730372348551029 ) ) ;
#42505=CARTESIAN_POINT ( 'NONE',  ( 6.020204320972966094, 1.861307952554195122, 7.572700244129132230 ) ) ;
#42773=CARTESIAN_POINT ( 'NONE',  ( 0.9126302363882010660, -2.499999999999998224, 9.000000000000003553 ) ) ;
#42827=B_SPLINE_CURVE_WITH_KNOTS ( 'NONE', 3,
 ( #58632, #15064, #62850, #9771, #53367, #26264, #63562, #47435 ),
 .UNSPECIFIED., .F., .F.,
 ( 4, 2, 2, 4 ),
 ( 0.005458618329390014547, 0.006805794425120373359, 0.008152970520850733038, 0.01084732271231145413 ),
 .UNSPECIFIED. ) ;
#42840=AXIS2_PLACEMENT_3D ( 'NONE', #59977, #7217, #49786 ) ;
#43071=DIRECTION ( 'NONE',  ( 0.000000000000000000, 0.000000000000000000, 1.000000000000000000 ) ) ;
#43211=FILL_AREA_STYLE_COLOUR ( '', #55752 ) ;
#43314=DIRECTION ( 'NONE',  ( 0.000000000000000000, 0.000000000000000000, 1.000000000000000000 ) ) ;
#43339=VERTEX_POINT ( 'NONE', #64030 ) ;
#43517=CIRCLE ( 'NONE', #17682, 5.500000000000005329 ) ;
#43657=EDGE_CURVE ( 'NONE', #67877, #60124, #10700, .T. ) ;
#43667=CARTESIAN_POINT ( 'NONE',  ( -7.794228634059947147, 2.500000000000000000, -4.500000000000000000 ) ) ;
#43888=STYLED_ITEM ( 'NONE', ( #61275 ), #12828 ) ;
#43988=CARTESIAN_POINT ( 'NONE',  ( -7.566679973970432016, -2.499999999999994671, -4.894125840469273570 ) ) ;
#44019=CIRCLE ( 'NONE', #1218, 5.500000000000001776 ) ;
#44070=CARTESIAN_POINT ( 'NONE',  ( 0.000000000000000000, -2.500000000000000000, 0.000000000000000000 ) ) ;
#44094=CARTESIAN_POINT ( 'NONE',  ( -7.342319042881618962, 2.499999999999994671, 5.282730372348551029 ) ) ;
#44223=CONICAL_SURFACE ( 'NONE', #11584, 9.000000000000000000, 0.7853981633974500554 ) ;
#44361=LINE ( 'NONE', #39410, #32900 ) ;
#44434=ORIENTED_EDGE ( 'NONE', *, *, #25721, .F. ) ;
#44482=ORIENTED_EDGE ( 'NONE', *, *, #19275, .F. ) ;
#44685=B_SPLINE_CURVE_WITH_KNOTS ( 'NONE', 3,
 ( #26784, #48313, #7, #704, #54233, #6053 ),
 .UNSPECIFIED., .F., .F.,
 ( 4, 2, 4 ),
 ( 0.005386537104126975541, 0.008060814333094815098, 0.01073509156206265379 ),
 .UNSPECIFIED. ) ;
#44958=CARTESIAN_POINT ( 'NONE',  ( 8.920833891111493941, -2.231456886122029193, -2.548662454712524728 ) ) ;
#45154=EDGE_CURVE ( 'NONE', #60124, #22316, #6792, .T. ) ;
#45263=EDGE_CURVE ( 'NONE', #47020, #59162, #51829, .T. ) ;
#45453=ORIENTED_EDGE ( 'NONE', *, *, #68284, .T. ) ;
#45556=VERTEX_POINT ( 'NONE', #4437 ) ;
#45575=EDGE_CURVE ( 'NONE', #39293, #36711, #16098, .T. ) ;
#45825=( NAMED_UNIT ( * ) SI_UNIT ( $, .STERADIAN. ) SOLID_ANGLE_UNIT ( ) );
#45882=B_SPLINE_CURVE_WITH_KNOTS ( 'NONE', 3,
 ( #55487, #56163, #55829, #29068, #50566, #2291, #7992, #29437 ),
 .UNSPECIFIED., .F., .F.,
 ( 4, 2, 2, 4 ),
 ( 2.544313220892526165E-07, 0.002693395767724534023, 0.004039966435925755432, 0.005386537104126977275 ),
 .UNSPECIFIED. ) ;
#45956=DIRECTION ( 'NONE',  ( 0.000000000000000000, 1.000000000000000000, 0.000000000000000000 ) ) ;
#45959=ORIENTED_EDGE ( 'NONE', *, *, #41987, .F. ) ;
#45993=UNCERTAINTY_MEASURE_WITH_UNIT (LENGTH_MEASURE( 1.000000000000000082E-05 ), #66920, 'distance_accuracy_value', 'NONE');
#46007=CARTESIAN_POINT ( 'NONE',  ( -4.390521455347699664, -1.510510638266201466, -9.000000000000003553 ) ) ;
#46131=LINE ( 'NONE', #34840, #55907 ) ;
#46367=CARTESIAN_POINT ( 'NONE',  ( -1.585182400056157181, -2.380245935246553035, -9.000000000000005329 ) ) ;
#46390=LINE ( 'NONE', #35098, #16468 ) ;
#46399=CARTESIAN_POINT ( 'NONE',  ( 7.794228634059945371, 2.500000000000000000, 4.500000000000000888 ) ) ;
#46426=CARTESIAN_POINT ( 'NONE',  ( -10.39230484541326938, 1.107695154586735509, -1.661048719744147042E-15 ) ) ;
#46543=( NAMED_UNIT ( * ) PLANE_ANGLE_UNIT ( ) SI_UNIT ( $, .RADIAN. ) );
#46565=ORIENTED_EDGE ( 'NONE', *, *, #8979, .T. ) ;
#46681=CARTESIAN_POINT ( 'NONE',  ( 0.000000000000000000, 1.999999999999998668, 0.000000000000000000 ) ) ;
#46692=EDGE_CURVE ( 'NONE', #4344, #28673, #8821, .T. ) ;
#46787=FACE_OUTER_BOUND ( 'NONE', #66423, .T. ) ;
#46816=VERTEX_POINT ( 'NONE', #55708 ) ;
#46924=CARTESIAN_POINT ( 'NONE',  ( 0.000000000000000000, -2.500000000000000000, 0.000000000000000000 ) ) ;
#46934=CARTESIAN_POINT ( 'NONE',  ( -5.196152422706636465, 2.500000000000000000, 9.000000000000001776 ) ) ;
#46992=CARTESIAN_POINT ( 'NONE',  ( 7.794228634059945371, -2.500000000000000000, 4.500000000000000888 ) ) ;
#47020=VERTEX_POINT ( 'NONE', #9960 ) ;
#47282=VERTEX_POINT ( 'NONE', #37689 ) ;
#47435=CARTESIAN_POINT ( 'NONE',  ( -1.502314598737159031E-15, 2.500000000000000000, -9.000000000000000000 ) ) ;
#47598=DIRECTION ( 'NONE',  ( -0.000000000000000000, -1.000000000000000000, -0.000000000000000000 ) ) ;
#47614=AXIS2_PLACEMENT_3D ( 'NONE', #17629, #34121, #2766 ) ;
#47619=DIRECTION ( 'NONE',  ( 0.000000000000000000, -0.000000000000000000, 1.000000000000000000 ) ) ;
#47740=CARTESIAN_POINT ( 'NONE',  ( -8.246138225238285102, 2.499999999999994671, -3.717269627651451191 ) ) ;
#47805=( LENGTH_UNIT ( ) NAMED_UNIT ( * ) SI_UNIT ( .MILLI., .METRE. ) );
#47813=CARTESIAN_POINT ( 'NONE',  ( 5.603568002170370654, 1.515110734050476804, 8.294335516573690725 ) ) ;
#47834=PLANE ( 'NONE',  #26408 ) ;
#47872=APPLICATION_CONTEXT ( 'automotive_design' ) ;
#47915=ORIENTED_EDGE ( 'NONE', *, *, #8979, .F. ) ;
#48096=UNCERTAINTY_MEASURE_WITH_UNIT (LENGTH_MEASURE( 1.000000000000000082E-05 ), #3170, 'distance_accuracy_value', 'NONE');
#48222=CARTESIAN_POINT ( 'NONE',  ( -7.335726704534230258, -2.464278740834323411, -5.294148637306920868 ) ) ;
#48309=UNCERTAINTY_MEASURE_WITH_UNIT (LENGTH_MEASURE( 1.000000000000000082E-05 ), #47805, 'distance_accuracy_value', 'NONE');
#48313=CARTESIAN_POINT ( 'NONE',  ( 8.246138225238281549, -2.499999999999997780, 3.717269627651450303 ) ) ;
#48330=CARTESIAN_POINT ( 'NONE',  ( 0.000000000000000000, 2.500000000000000000, 0.000000000000000000 ) ) ;
#48555=ORIENTED_EDGE ( 'NONE', *, *, #64162, .T. ) ;
#48601=EDGE_CURVE ( 'NONE', #43339, #22316, #63985, .T. ) ;
#48621=VECTOR ( 'NONE', #49321, 1000.000000000000000 ) ;
#48717=ORIENTED_EDGE ( 'NONE', *, *, #9222, .T. ) ;
#48738=ORIENTED_EDGE ( 'NONE', *, *, #12220, .F. ) ;
#48849=CARTESIAN_POINT ( 'NONE',  ( 0.000000000000000000, -2.500000000000000000, 0.000000000000000000 ) ) ;
#48927=CARTESIAN_POINT ( 'NONE',  ( -5.196152422706636465, -1.107695154586736175, -9.000000000000003553 ) ) ;
#48943=CARTESIAN_POINT ( 'NONE',  ( -5.196152422706636465, 2.500000000000000000, -9.000000000000003553 ) ) ;
#48965=ADVANCED_FACE ( 'NONE', ( #59372 ), #28557, .T. ) ;
#48986=CARTESIAN_POINT ( 'NONE',  ( -2.243484957755116138, 2.233878551459168360, -9.000000000000003553 ) ) ;
#48987=PLANE ( 'NONE',  #26437 ) ;
#49011=ORIENTED_EDGE ( 'NONE', *, *, #33123, .F. ) ;
#49054=DIRECTION ( 'NONE',  ( 0.000000000000000000, 0.000000000000000000, 1.000000000000000000 ) ) ;
#49153=CARTESIAN_POINT ( 'NONE',  ( 7.794228634059946259, 2.500000000000000000, -4.500000000000001776 ) ) ;
#49266=EDGE_CURVE ( 'NONE', #39293, #33880, #65794, .T. ) ;
#49296=CARTESIAN_POINT ( 'NONE',  ( -0.4575609230677349926, 2.491211107078686648, -9.000000000000003553 ) ) ;
#49321=DIRECTION ( 'NONE',  ( -0.000000000000000000, -1.000000000000000000, -0.000000000000000000 ) ) ;
#49338=ORIENTED_EDGE ( 'NONE', *, *, #45575, .F. ) ;
#49339=CIRCLE ( 'NONE', #63921, 9.000000000000000000 ) ;
#49446=AXIS2_PLACEMENT_3D ( 'NONE', #7383, #39419, #39767 ) ;
#49465=CIRCLE ( 'NONE', #19104, 9.000000000000000000 ) ;
#49490=EDGE_CURVE ( 'NONE', #33880, #60416, #2605, .T. ) ;
#49662=EDGE_CURVE ( 'NONE', #51850, #63169, #55512, .T. ) ;
#49682=CARTESIAN_POINT ( 'NONE',  ( -5.603096392576914830, 1.514639124457109354, 8.295152368350901639 ) ) ;
#49786=DIRECTION ( 'NONE',  ( 1.000000000000000000, 0.000000000000000000, 0.000000000000000000 ) ) ;
#49834=ORIENTED_EDGE ( 'NONE', *, *, #60685, .F. ) ;
#49853=CARTESIAN_POINT ( 'NONE',  ( 7.342319042881613633, -2.499999999999998224, -5.282730372348551029 ) ) ;
#49857=AXIS2_PLACEMENT_3D ( 'NONE', #9228, #3540, #35958 ) ;
#49919=CARTESIAN_POINT ( 'NONE',  ( -9.566487832665403701, -1.863712308906138704, -1.430357023834059271 ) ) ;
#50167=FACE_OUTER_BOUND ( 'NONE', #61836, .T. ) ;
#50196=CARTESIAN_POINT ( 'NONE',  ( 6.021969435454494146, -1.863712308906143589, -7.569642976165943615 ) ) ;
#50425=ORIENTED_EDGE ( 'NONE', *, *, #40622, .T. ) ;
#50500=CYLINDRICAL_SURFACE ( 'NONE', #61174, 5.000000000000000000 ) ;
#50555=CARTESIAN_POINT ( 'NONE',  ( 10.39230484541326582, -1.107695154586738839, 1.440973567693753677E-18 ) ) ;
#50566=CARTESIAN_POINT ( 'NONE',  ( 8.701243704650551081, 2.329718218673044738, -2.929003814506405678 ) ) ;
#50576=CARTESIAN_POINT ( 'NONE',  ( 5.196152422706631135, 1.107695154586740394, 9.000000000000001776 ) ) ;
#50701=VECTOR ( 'NONE', #37580, 1000.000000000000000 ) ;
#50780=AXIS2_PLACEMENT_3D ( 'NONE', #10317, #26120, #62703 ) ;
#50853=CIRCLE ( 'NONE', #2486, 5.000000000000000000 ) ;
#51112=ORIENTED_EDGE ( 'NONE', *, *, #49662, .T. ) ;
#51134=DIRECTION ( 'NONE',  ( -0.000000000000000000, -1.000000000000000000, -0.000000000000000000 ) ) ;
#51190=VECTOR ( 'NONE', #8978, 1000.000000000000000 ) ;
#51196=EDGE_LOOP ( 'NONE', ( #35792, #21531, #51710 ) ) ;
#51263=CARTESIAN_POINT ( 'NONE',  ( -2.243484957755116138, -2.233878551459168360, -9.000000000000003553 ) ) ;
#51364=ORIENTED_EDGE ( 'NONE', *, *, #29472, .F. ) ;
#51423=SURFACE_STYLE_FILL_AREA ( #2841 ) ;
#51703=DIRECTION ( 'NONE',  ( 0.000000000000000000, -1.000000000000000000, 0.000000000000000000 ) ) ;
#51710=ORIENTED_EDGE ( 'NONE', *, *, #48601, .F. ) ;
#51765=ORIENTED_EDGE ( 'NONE', *, *, #11741, .F. ) ;
#51803=LINE ( 'NONE', #8877, #510 ) ;
#51829=B_SPLINE_CURVE_WITH_KNOTS ( 'NONE', 3,
 ( #27461, #27794, #49296, #59838, #39116, #48986, #60185, #16613, #37752 ),
 .UNSPECIFIED., .F., .F.,
 ( 4, 2, 1, 2, 4 ),
 ( 0.01084732271231145413, 0.01152005980350376095, 0.01219279689469606777, 0.01353827107708068141, 0.01622921944184991042 ),
 .UNSPECIFIED. ) ;
#51850=VERTEX_POINT ( 'NONE', #26574 ) ;
#52004=CARTESIAN_POINT ( 'NONE',  ( 5.196152422706631135, 2.500000000000000000, 9.000000000000001776 ) ) ;
#52133=DIRECTION ( 'NONE',  ( -0.4999999999999998890, 0.000000000000000000, -0.8660254037844385966 ) ) ;
#52214=CIRCLE ( 'NONE', #21866, 5.500000000000001776 ) ;
#52220=AXIS2_PLACEMENT_3D ( 'NONE', #64688, #27010, #31972 ) ;
#52248=DIRECTION ( 'NONE',  ( 0.000000000000000000, 0.000000000000000000, 1.000000000000000000 ) ) ;
#52251=VERTEX_POINT ( 'NONE', #24091 ) ;
#52335=CARTESIAN_POINT ( 'NONE',  ( 7.794228634059945371, -2.500000000000000000, 4.500000000000000888 ) ) ;
#52392=ADVANCED_FACE ( 'NONE', ( #20187 ), #55111, .T. ) ;
#52437=ADVANCED_FACE ( 'NONE', ( #22980 ), #6093, .F. ) ;
#52586=ORIENTED_EDGE ( 'NONE', *, *, #30975, .F. ) ;
#52592=CARTESIAN_POINT ( 'NONE',  ( 5.603568002170370654, -1.515110734050476804, 8.294335516573690725 ) ) ;
#52878=ORIENTED_EDGE ( 'NONE', *, *, #49490, .F. ) ;
#52912=CONICAL_SURFACE ( 'NONE', #36094, 9.000000000000000000, 0.7853981633974500554 ) ;
#52999=DIRECTION ( 'NONE',  ( 0.000000000000000000, -0.000000000000000000, 1.000000000000000000 ) ) ;
#53048=AXIS2_PLACEMENT_3D ( 'NONE', #12422, #51134, #7848 ) ;
#53065=CARTESIAN_POINT ( 'NONE',  ( -0.2278693232858663154, -2.499999999999997780, 9.000000000000003553 ) ) ;
#53100=CARTESIAN_POINT ( 'NONE',  ( -8.021777294149472937, -2.499999999999994227, 4.105874159530730871 ) ) ;
#53128=FACE_OUTER_BOUND ( 'NONE', #10893, .T. ) ;
#53131=CARTESIAN_POINT ( 'NONE',  ( 0.000000000000000000, -2.500000000000000000, 0.000000000000000000 ) ) ;
#53343=CARTESIAN_POINT ( 'NONE',  ( -5.196152422706636465, -1.107695154586737063, 9.000000000000001776 ) ) ;
#53362=VERTEX_POINT ( 'NONE', #22619 ) ;
#53367=CARTESIAN_POINT ( 'NONE',  ( 3.109477999331718312, 1.987149502472170370, -9.000000000000005329 ) ) ;
#53585=B_SPLINE_CURVE_WITH_KNOTS ( 'NONE', 3,
 ( #21242, #42773, #5404, #16370, #59217, #27199, #59575, #11392 ),
 .UNSPECIFIED., .F., .F.,
 ( 4, 2, 2, 4 ),
 ( 0.01462827986756859780, 0.01731435831274189333, 0.01865739753532854109, 0.02000043675791518885 ),
 .UNSPECIFIED. ) ;
#53612=VERTEX_POINT ( 'NONE', #21754 ) ;
#53633=CARTESIAN_POINT ( 'NONE',  ( -10.39230484541326938, 1.107695154586735509, -1.661048719744147042E-15 ) ) ;
#53685=DIRECTION ( 'NONE',  ( -0.000000000000000000, -1.000000000000000000, -0.000000000000000000 ) ) ;
#53693=ORIENTED_EDGE ( 'NONE', *, *, #49662, .F. ) ;
#53771=CARTESIAN_POINT ( 'NONE',  ( 9.566487832665400148, 1.863712308906143811, 1.430357023834058161 ) ) ;
#54039=FILL_AREA_STYLE ('',( #43211 ) ) ;
#54125=ORIENTED_EDGE ( 'NONE', *, *, #57091, .T. ) ;
#54233=CARTESIAN_POINT ( 'NONE',  ( 9.985360875542987458, -1.514639124457112018, 0.7048476316490990268 ) ) ;
#54294=FACE_OUTER_BOUND ( 'NONE', #21173, .T. ) ;
#54328=CONICAL_SURFACE ( 'NONE', #59998, 5.500000000000005329, 0.7853981633974482790 ) ;
#54388=CARTESIAN_POINT ( 'NONE',  ( 0.000000000000000000, -2.500000000000000000, 0.000000000000000000 ) ) ;
#54514=CARTESIAN_POINT ( 'NONE',  ( -5.196152422706636465, 1.107695154586736175, -9.000000000000003553 ) ) ;
#54616=ORIENTED_EDGE ( 'NONE', *, *, #62164, .T. ) ;
#54671=EDGE_CURVE ( 'NONE', #60124, #43339, #53585, .T. ) ;
#54766=DIRECTION ( 'NONE',  ( 0.000000000000000000, 1.000000000000000000, 0.000000000000000000 ) ) ;
#54889=ORIENTED_EDGE ( 'NONE', *, *, #57091, .F. ) ;
#54912=CARTESIAN_POINT ( 'NONE',  ( -7.794228634059948035, 2.500000000000000000, 4.499999999999999112 ) ) ;
#54950=CIRCLE ( 'NONE', #5390, 9.000000000000000000 ) ;
#55093=CARTESIAN_POINT ( 'NONE',  ( 7.794228634059946259, -2.500000000000000000, -4.500000000000001776 ) ) ;
#55111=CONICAL_SURFACE ( 'NONE', #31513, 9.000000000000000000, 0.7853981633974500554 ) ;
#55197=CARTESIAN_POINT ( 'NONE',  ( -7.566679973970432016, 2.499999999999994671, -4.894125840469273570 ) ) ;
#55285=ADVANCED_FACE ( 'NONE', ( #53128 ), #44223, .T. ) ;
#55431=ORIENTED_EDGE ( 'NONE', *, *, #42162, .F. ) ;
#55487=CARTESIAN_POINT ( 'NONE',  ( 10.39230484541326582, 1.107695154586738839, 1.440973567693753677E-18 ) ) ;
#55512=B_SPLINE_CURVE_WITH_KNOTS ( 'NONE', 3,
 ( #57873, #31804, #14600, #25486, #20925, #58545, #42422, #3654 ),
 .UNSPECIFIED., .F., .F.,
 ( 4, 2, 2, 4 ),
 ( 0.005458618329390014547, 0.006805794425120373359, 0.008152970520850733038, 0.01084732271231145413 ),
 .UNSPECIFIED. ) ;
#55606=DIRECTION ( 'NONE',  ( -0.000000000000000000, -1.000000000000000000, -0.000000000000000000 ) ) ;
#55636=EDGE_LOOP ( 'NONE', ( #11118, #17168, #6772, #1549 ) ) ;
#55646=ORIENTED_EDGE ( 'NONE', *, *, #12640, .F. ) ;
#55708=CARTESIAN_POINT ( 'NONE',  ( 7.794228634059946259, 2.500000000000000000, -4.500000000000001776 ) ) ;
#55749=B_SPLINE_CURVE_WITH_KNOTS ( 'NONE', 3,
 ( #48927, #22144, #32341, #21103, #625, #48222, #43988, #11580 ),
 .UNSPECIFIED., .F., .F.,
 ( 4, 2, 2, 4 ),
 ( 2.544313220903533887E-07, 0.002693395767724532288, 0.004039966435925753697, 0.005386537104126974673 ),
 .UNSPECIFIED. ) ;
#55752=COLOUR_RGB ( '', 0.66274510, 0.83137255, 0.94901961) ;
#55829=CARTESIAN_POINT ( 'NONE',  ( 9.568252947146927312, 1.861307952554195566, -1.427299755870872433 ) ) ;
#55845=CARTESIAN_POINT ( 'NONE',  ( 1.802043943559354711, 2.359472279213376211, 9.000000000000003553 ) ) ;
#55907=VECTOR ( 'NONE', #62951, 1000.000000000000114 ) ;
#56048=EDGE_CURVE ( 'NONE', #8712, #53612, #41780, .T. ) ;
#56163=CARTESIAN_POINT ( 'NONE',  ( 9.984889265949528081, 1.515110734050476582, -0.7056644834263100519 ) ) ;
#56277=ORIENTED_EDGE ( 'NONE', *, *, #45263, .T. ) ;
#56339=SURFACE_SIDE_STYLE ('',( #51423 ) ) ;
#56519=CIRCLE ( 'NONE', #47614, 9.000000000000000000 ) ;
#56545=DIRECTION ( 'NONE',  ( -0.000000000000000000, -1.000000000000000000, -0.000000000000000000 ) ) ;
#56743=ADVANCED_FACE ( 'NONE', ( #6024, #27462 ), #48987, .T. ) ;
#56753=FACE_OUTER_BOUND ( 'NONE', #19244, .T. ) ;
#56915=VERTEX_POINT ( 'NONE', #35882 ) ;
#56975=CARTESIAN_POINT ( 'NONE',  ( -7.794228634059948035, -2.500000000000000000, 4.499999999999999112 ) ) ;
#57091=EDGE_CURVE ( 'NONE', #28673, #66441, #60910, .T. ) ;
#57341=AXIS2_PLACEMENT_3D ( 'NONE', #33854, #65882, #5730 ) ;
#57367=EDGE_LOOP ( 'NONE', ( #34046, #44434, #28918 ) ) ;
#57478=CIRCLE ( 'NONE', #67579, 5.500000000000005329 ) ;
#57531=ORIENTED_EDGE ( 'NONE', *, *, #24751, .F. ) ;
#57631=CARTESIAN_POINT ( 'NONE',  ( 10.39230484541326582, 2.500000000000000000, 0.000000000000000000 ) ) ;
#57843=B_SPLINE_CURVE_WITH_KNOTS ( 'NONE', 3,
 ( #37317, #10545, #31984, #5239, #26682, #66414, #8019, #66772, #40073, #61804 ),
 .UNSPECIFIED., .F., .F.,
 ( 4, 2, 2, 2, 4 ),
 ( 0.009262909725840906203, 0.01194559479670475113, 0.01328693733213667447, 0.01395760859985263613, 0.01462827986756859780 ),
 .UNSPECIFIED. ) ;
#57856=DIRECTION ( 'NONE',  ( -0.000000000000000000, -1.000000000000000000, -0.000000000000000000 ) ) ;
#57871=B_SPLINE_CURVE_WITH_KNOTS ( 'NONE', 3,
 ( #54912, #44094, #33155, #6740, #49682, #39150 ),
 .UNSPECIFIED., .F., .F.,
 ( 4, 2, 4 ),
 ( 0.005386537104126977275, 0.008060814333094816833, 0.01073509156206265552 ),
 .UNSPECIFIED. ) ;
#57873=CARTESIAN_POINT ( 'NONE',  ( 5.196152422706628471, -1.107695154586738173, -9.000000000000005329 ) ) ;
#57878=ORIENTED_EDGE ( 'NONE', *, *, #45263, .F. ) ;
#57915=B_SPLINE_CURVE_WITH_KNOTS ( 'NONE', 3,
 ( #3723, #3360, #20638, #57941, #46367, #51263, #3008, #46007, #19927 ),
 .UNSPECIFIED., .F., .F.,
 ( 4, 2, 1, 2, 4 ),
 ( 0.01084732271231145413, 0.01152005980350376095, 0.01219279689469606777, 0.01353827107708068141, 0.01622921944184991042 ),
 .UNSPECIFIED. ) ;
#57917=CARTESIAN_POINT ( 'NONE',  ( -5.196152422706636465, 1.107695154586737063, 9.000000000000001776 ) ) ;
#57941=CARTESIAN_POINT ( 'NONE',  ( -0.9109038252169214811, -2.456844516558468694, -9.000000000000003553 ) ) ;
#58005=CARTESIAN_POINT ( 'NONE',  ( -5.196152422706636465, -1.107695154586737063, 9.000000000000001776 ) ) ;
#58216=FACE_OUTER_BOUND ( 'NONE', #9588, .T. ) ;
#58255=CARTESIAN_POINT ( 'NONE',  ( -6.898093598910797652, -2.361802048420727385, 6.052151411320861207 ) ) ;
#58262=DIRECTION ( 'NONE',  ( -0.000000000000000000, -1.000000000000000000, -0.000000000000000000 ) ) ;
#58545=CARTESIAN_POINT ( 'NONE',  ( 1.802043943559349604, -2.359472279213374435, -9.000000000000007105 ) ) ;
#58572=EDGE_CURVE ( 'NONE', #39293, #35271, #4106, .T. ) ;
#58610=DIRECTION ( 'NONE',  ( 0.000000000000000000, 1.000000000000000000, 0.000000000000000000 ) ) ;
#58632=CARTESIAN_POINT ( 'NONE',  ( 5.196152422706628471, 1.107695154586738173, -9.000000000000005329 ) ) ;
#58642=CARTESIAN_POINT ( 'NONE',  ( 7.335726704534224041, 2.464278740834329184, 5.294148637306918204 ) ) ;
#58666=EDGE_LOOP ( 'NONE', ( #47915, #11759, #40878 ) ) ;
#58769=EDGE_CURVE ( 'NONE', #46816, #29086, #63283, .T. ) ;
#58782=LINE ( 'NONE', #14847, #24197 ) ;
#58936=CARTESIAN_POINT ( 'NONE',  ( -7.794228634059947147, 2.500000000000000000, -4.500000000000000000 ) ) ;
#59061=CARTESIAN_POINT ( 'NONE',  ( 7.794228634059945371, 2.500000000000000000, 4.500000000000000888 ) ) ;
#59162=VERTEX_POINT ( 'NONE', #9548 ) ;
#59217=CARTESIAN_POINT ( 'NONE',  ( 3.542752237027638085, -1.835478060177118120, 9.000000000000003553 ) ) ;
#59299=SURFACE_STYLE_USAGE ( .BOTH. , #37925 ) ;
#59339=CARTESIAN_POINT ( 'NONE',  ( -2.243484957755116582, -2.233878551459170136, 9.000000000000005329 ) ) ;
#59372=FACE_OUTER_BOUND ( 'NONE', #19424, .T. ) ;
#59466=EDGE_LOOP ( 'NONE', ( #66581, #17995, #17844, #65457 ) ) ;
#59575=CARTESIAN_POINT ( 'NONE',  ( 4.793834890952475725, -1.308853920463818987, 9.000000000000005329 ) ) ;
#59838=CARTESIAN_POINT ( 'NONE',  ( -0.9109038252169214811, 2.456844516558468694, -9.000000000000003553 ) ) ;
#59840=ADVANCED_FACE ( 'NONE', ( #17858 ), #52912, .T. ) ;
#59977=CARTESIAN_POINT ( 'NONE',  ( 0.000000000000000000, 0.000000000000000000, 0.000000000000000000 ) ) ;
#59998=AXIS2_PLACEMENT_3D ( 'NONE', #2645, #33325, #1240 ) ;
#60021=CARTESIAN_POINT ( 'NONE',  ( 7.342319042881613633, 2.499999999999998224, -5.282730372348551029 ) ) ;
#60101=CARTESIAN_POINT ( 'NONE',  ( -9.985360875542991010, -1.514639124457108244, -0.7048476316491002480 ) ) ;
#60124=VERTEX_POINT ( 'NONE', #18721 ) ;
#60185=CARTESIAN_POINT ( 'NONE',  ( -3.542344102440325049, 1.863645424029197750, -9.000000000000007105 ) ) ;
#60416=VERTEX_POINT ( 'NONE', #17630 ) ;
#60424=ORIENTED_EDGE ( 'NONE', *, *, #3028, .T. ) ;
#60465=ORIENTED_EDGE ( 'NONE', *, *, #26453, .F. ) ;
#60612=ORIENTED_EDGE ( 'NONE', *, *, #24751, .T. ) ;
#60685=EDGE_CURVE ( 'NONE', #36711, #60416, #20460, .T. ) ;
#60829=EDGE_CURVE ( 'NONE', #63169, #23616, #57915, .T. ) ;
#60910=B_SPLINE_CURVE_WITH_KNOTS ( 'NONE', 3,
 ( #59061, #4542, #9852, #53771, #15489, #5572 ),
 .UNSPECIFIED., .F., .F.,
 ( 4, 2, 4 ),
 ( 0.005386537104126975541, 0.008060814333094815098, 0.01073509156206265379 ),
 .UNSPECIFIED. ) ;
#60930=CARTESIAN_POINT ( 'NONE',  ( 0.000000000000000000, 2.500000000000000000, 0.000000000000000000 ) ) ;
#61091=CARTESIAN_POINT ( 'NONE',  ( 8.021777294149467608, -2.499999999999998224, -4.105874159530731760 ) ) ;
#61140=CARTESIAN_POINT ( 'NONE',  ( -8.690363669209109077, -2.361802048420726496, -2.947848588679145454 ) ) ;
#61174=AXIS2_PLACEMENT_3D ( 'NONE', #1557, #39979, #12854 ) ;
#61275=PRESENTATION_STYLE_ASSIGNMENT (( #40192 ) ) ;
#61420=CARTESIAN_POINT ( 'NONE',  ( 7.794228634059946259, -2.500000000000000000, -4.500000000000001776 ) ) ;
#61503=CIRCLE ( 'NONE', #7638, 5.000000000000000000 ) ;
#61532=EDGE_CURVE ( 'NONE', #18297, #56915, #12525, .T. ) ;
#61757=ORIENTED_EDGE ( 'NONE', *, *, #58769, .T. ) ;
#61786=( GEOMETRIC_REPRESENTATION_CONTEXT ( 3 ) GLOBAL_UNCERTAINTY_ASSIGNED_CONTEXT ( ( #45993 ) ) GLOBAL_UNIT_ASSIGNED_CONTEXT ( ( #66920, #25376, #13083 ) ) REPRESENTATION_CONTEXT ( 'NONE', 'WORKASPACE' ) );
#61804=CARTESIAN_POINT ( 'NONE',  ( 0.000000000000000000, 2.500000000000000000, 9.000000000000001776 ) ) ;
#61836=EDGE_LOOP ( 'NONE', ( #49338, #30934, #26198, #19608 ) ) ;
#62030=ADVANCED_FACE ( 'NONE', ( #50167 ), #50500, .F. ) ;
#62056=B_SPLINE_CURVE_WITH_KNOTS ( 'NONE', 3,
 ( #50555, #23451, #19204, #44958, #67074, #66364, #61091, #61420 ),
 .UNSPECIFIED., .F., .F.,
 ( 4, 2, 2, 4 ),
 ( 2.544313220892526165E-07, 0.002693395767724534023, 0.004039966435925755432, 0.005386537104126977275 ),
 .UNSPECIFIED. ) ;
#62078=DIRECTION ( 'NONE',  ( 8.659560562354932858E-17, -0.7071067811865474617, 0.7071067811865474617 ) ) ;
#62139=AXIS2_PLACEMENT_3D ( 'NONE', #46924, #63039, #3937 ) ;
#62164=EDGE_CURVE ( 'NONE', #13621, #63169, #63444, .T. ) ;
#62385=ADVANCED_FACE ( 'NONE', ( #54294 ), #37682, .T. ) ;
#62452=DIRECTION ( 'NONE',  ( 0.000000000000000000, 0.000000000000000000, 1.000000000000000000 ) ) ;
#62631=DIRECTION ( 'NONE',  ( 0.000000000000000000, 0.000000000000000000, 1.000000000000000000 ) ) ;
#62703=DIRECTION ( 'NONE',  ( 0.000000000000000000, 0.000000000000000000, 1.000000000000000000 ) ) ;
#62850=CARTESIAN_POINT ( 'NONE',  ( 4.383776131304275125, 1.496531397472843361, -9.000000000000007105 ) ) ;
#62864=EDGE_LOOP ( 'NONE', ( #21854, #12226 ) ) ;
#62951=DIRECTION ( 'NONE',  ( 0.000000000000000000, 0.7071067811865474617, 0.7071067811865474617 ) ) ;
#63039=DIRECTION ( 'NONE',  ( -0.000000000000000000, 1.000000000000000000, -0.000000000000000000 ) ) ;
#63112=LINE ( 'NONE', #24764, #13435 ) ;
#63169=VERTEX_POINT ( 'NONE', #2462 ) ;
#63283=B_SPLINE_CURVE_WITH_KNOTS ( 'NONE', 3,
 ( #49153, #60021, #33637, #17149, #28331, #6216 ),
 .UNSPECIFIED., .F., .F.,
 ( 4, 2, 4 ),
 ( 0.005386537104126977275, 0.008060814333094818568, 0.01073509156206266073 ),
 .UNSPECIFIED. ) ;
#63296=CARTESIAN_POINT ( 'NONE',  ( -9.984889265949528081, -1.515110734050472141, 0.7056644834263087196 ) ) ;
#63444=CIRCLE ( 'NONE', #67929, 9.000000000000000000 ) ;
#63462=EDGE_CURVE ( 'NONE', #52251, #36619, #52214, .T. ) ;
#63491=EDGE_LOOP ( 'NONE', ( #13647, #3724, #36769, #15281, #45959, #60465 ) ) ;
#63562=CARTESIAN_POINT ( 'NONE',  ( 0.9126302363881977353, 2.499999999999996447, -9.000000000000007105 ) ) ;
#63606=CARTESIAN_POINT ( 'NONE',  ( -3.542344102440326825, -1.863645424029198194, 9.000000000000000000 ) ) ;
#63621=ADVANCED_FACE ( 'NONE', ( #27750 ), #961, .F. ) ;
#63730=ORIENTED_EDGE ( 'NONE', *, *, #33286, .F. ) ;
#63910=CARTESIAN_POINT ( 'NONE',  ( 0.000000000000000000, 2.500000000000000000, 5.500000000000001776 ) ) ;
#63919=DIRECTION ( 'NONE',  ( 0.000000000000000000, 0.000000000000000000, 1.000000000000000000 ) ) ;
#63921=AXIS2_PLACEMENT_3D ( 'NONE', #26631, #68898, #27319 ) ;
#63985=B_SPLINE_CURVE_WITH_KNOTS ( 'NONE', 3,
 ( #20553, #52592, #36443, #30748, #41007, #26166, #3643, #46992 ),
 .UNSPECIFIED., .F., .F.,
 ( 4, 2, 2, 4 ),
 ( 2.544313220888523934E-07, 0.002693395767724531854, 0.004039966435925753697, 0.005386537104126975541 ),
 .UNSPECIFIED. ) ;
#64015=EDGE_LOOP ( 'NONE', ( #68239, #64849, #51364 ) ) ;
#64030=CARTESIAN_POINT ( 'NONE',  ( 5.196152422706631135, -1.107695154586740394, 9.000000000000001776 ) ) ;
#64094=CARTESIAN_POINT ( 'NONE',  ( 10.39230484541326582, 2.500000000000000000, 0.000000000000000000 ) ) ;
#64103=CARTESIAN_POINT ( 'NONE',  ( -10.39230484541326938, -1.107695154586735509, -1.661048719643172847E-15 ) ) ;
#64162=EDGE_CURVE ( 'NONE', #4344, #43339, #67970, .T. ) ;
#64291=CARTESIAN_POINT ( 'NONE',  ( -0.9109038252169192607, -2.456844516558473135, 9.000000000000001776 ) ) ;
#64346=EDGE_CURVE ( 'NONE', #29086, #51850, #58782, .T. ) ;
#64432=CONICAL_SURFACE ( 'NONE', #28444, 5.500000000000005329, 0.7853981633974482790 ) ;
#64568=B_SPLINE_CURVE_WITH_KNOTS ( 'NONE', 3,
 ( #12574, #33692, #55845, #39016, #66754, #7644, #28388, #50576 ),
 .UNSPECIFIED., .F., .F.,
 ( 4, 2, 2, 4 ),
 ( 0.01462827986756859780, 0.01731435831274189333, 0.01865739753532854109, 0.02000043675791518885 ),
 .UNSPECIFIED. ) ;
#64575=AXIS2_PLACEMENT_3D ( 'NONE', #11876, #566, #22091 ) ;
#64580=B_SPLINE_CURVE_WITH_KNOTS ( 'NONE', 3,
 ( #54514, #17273, #6323, #7381, #66099, #22518, #55197, #43667 ),
 .UNSPECIFIED., .F., .F.,
 ( 4, 2, 2, 4 ),
 ( 2.544313220903533887E-07, 0.002693395767724532288, 0.004039966435925753697, 0.005386537104126974673 ),
 .UNSPECIFIED. ) ;
#64641=EDGE_LOOP ( 'NONE', ( #3226, #51112, #6016, #28443, #57878, #30046 ) ) ;
#64661=FACE_OUTER_BOUND ( 'NONE', #36547, .T. ) ;
#64670=ADVANCED_FACE ( 'NONE', ( #40411 ), #66429, .F. ) ;
#64688=CARTESIAN_POINT ( 'NONE',  ( 0.000000000000000000, -2.500000000000000000, 0.000000000000000000 ) ) ;
#64849=ORIENTED_EDGE ( 'NONE', *, *, #26453, .T. ) ;
#64871=EDGE_LOOP ( 'NONE', ( #50425, #18771 ) ) ;
#65016=ORIENTED_EDGE ( 'NONE', *, *, #33593, .T. ) ;
#65198=CARTESIAN_POINT ( 'NONE',  ( 0.000000000000000000, 2.500000000000000000, 0.000000000000000000 ) ) ;
#65457=ORIENTED_EDGE ( 'NONE', *, *, #63462, .F. ) ;
#65794=CIRCLE ( 'NONE', #39970, 5.000000000000000000 ) ;
#65882=DIRECTION ( 'NONE',  ( 1.669238443041287922E-16, -0.000000000000000000, 1.000000000000000000 ) ) ;
#66099=CARTESIAN_POINT ( 'NONE',  ( -6.887213563469350319, 2.329718218673038077, -6.070996185493596542 ) ) ;
#66203=ORIENTED_EDGE ( 'NONE', *, *, #25721, .T. ) ;
#66364=CARTESIAN_POINT ( 'NONE',  ( 8.252730563585672030, -2.464278740834330517, -3.705851362693084905 ) ) ;
#66414=CARTESIAN_POINT ( 'NONE',  ( -1.135663242406173001, 2.431311185535292907, 9.000000000000003553 ) ) ;
#66423=EDGE_LOOP ( 'NONE', ( #60612, #39392, #6135, #39487, #27833, #63730 ) ) ;
#66429=PLANE ( 'NONE',  #26506 ) ;
#66441=VERTEX_POINT ( 'NONE', #33914 ) ;
#66581=ORIENTED_EDGE ( 'NONE', *, *, #29275, .F. ) ;
#66697=ORIENTED_EDGE ( 'NONE', *, *, #56048, .F. ) ;
#66754=CARTESIAN_POINT ( 'NONE',  ( 3.542752237027638085, 1.835478060177118120, 9.000000000000003553 ) ) ;
#66772=CARTESIAN_POINT ( 'NONE',  ( -0.4575609230677321060, 2.491211107078691089, 9.000000000000003553 ) ) ;
#66920=( LENGTH_UNIT ( ) NAMED_UNIT ( * ) SI_UNIT ( .MILLI., .METRE. ) );
#67074=CARTESIAN_POINT ( 'NONE',  ( 8.701243704650551081, -2.329718218673044738, -2.929003814506405678 ) ) ;
#67175=ORIENTED_EDGE ( 'NONE', *, *, #24418, .F. ) ;
#67176=DIRECTION ( 'NONE',  ( 0.000000000000000000, 0.000000000000000000, 1.000000000000000000 ) ) ;
#67371=LINE ( 'NONE', #2235, #18257 ) ;
#67579=AXIS2_PLACEMENT_3D ( 'NONE', #48849, #2551, #17169 ) ;
#67865=DIRECTION ( 'NONE',  ( 0.000000000000000000, 0.000000000000000000, 1.000000000000000000 ) ) ;
#67877=VERTEX_POINT ( 'NONE', #29611 ) ;
#67929=AXIS2_PLACEMENT_3D ( 'NONE', #24783, #2944, #29734 ) ;
#67970=LINE ( 'NONE', #28649, #33207 ) ;
#68239=ORIENTED_EDGE ( 'NONE', *, *, #56048, .T. ) ;
#68284=EDGE_CURVE ( 'NONE', #45556, #33218, #49339, .T. ) ;
#68684=CYLINDRICAL_SURFACE ( 'NONE', #62139, 5.000000000000000000 ) ;
#68695=DIRECTION ( 'NONE',  ( -1.000000000000000000, 0.000000000000000000, -0.000000000000000000 ) ) ;
#68790=CARTESIAN_POINT ( 'NONE',  ( 0.000000000000000000, -2.500000000000000000, 0.000000000000000000 ) ) ;
#68898=DIRECTION ( 'NONE',  ( 0.000000000000000000, 1.000000000000000000, 0.000000000000000000 ) ) ;
#69016=ORIENTED_EDGE ( 'NONE', *, *, #9222, .F. ) ;
#69137=CARTESIAN_POINT ( 'NONE',  ( -8.690363669209109077, 2.361802048420726496, -2.947848588679145454 ) ) ;
#69158=ADVANCED_FACE ( 'NONE', ( #12993 ), #69599, .F. ) ;
#69263=EDGE_CURVE ( 'NONE', #56915, #13621, #26938, .T. ) ;
#69274=CARTESIAN_POINT ( 'NONE',  ( -8.252730563585672030, -2.464278740834326520, 3.705851362693083573 ) ) ;
#69315=ORIENTED_EDGE ( 'NONE', *, *, #3028, .F. ) ;
#69518=DIRECTION ( 'NONE',  ( 0.000000000000000000, 0.000000000000000000, 1.000000000000000000 ) ) ;
#69562=DIRECTION ( 'NONE',  ( -0.000000000000000000, -1.000000000000000000, -0.000000000000000000 ) ) ;
#69599=CONICAL_SURFACE ( 'NONE', #49446, 5.000000000000000000, 0.7853981633974482790 ) ;
#69693=LINE ( 'NONE', #64094, #48621 ) ;
ENDSEC;
END-ISO-10303-21;
